ISO-10303-21;
HEADER;
/* Generated by software containing ST-Developer
 * from STEP Tools, Inc. (www.steptools.com) 
 */

FILE_DESCRIPTION(
/* description */ ('Independent compact industrial fixture table, bolted aluminum worktop
 on connected adjustable support base. Whole-mm nominal dimensions. No
 load rating assigned.'),
/* implementation_level */ '2;1');

FILE_NAME(
/* name */ 'Lock nut M10.step',
/* time_stamp */ '2026-11-07T17:47:58-08:00',
/* author */ (''),
/* organization */ (''),
/* preprocessor_version */ 'ST-DEVELOPER v20.2',
/* originating_system */ 'Autodesk Translation Framework v15.17.0.0',
/* authorisation */ '');

FILE_SCHEMA (('AUTOMOTIVE_DESIGN { 1 0 10303 214 3 1 1 }'));
ENDSEC;

DATA;
#10=MECHANICAL_DESIGN_GEOMETRIC_PRESENTATION_REPRESENTATION('',(#2262),#97475);
#358=B_SPLINE_SURFACE_WITH_KNOTS('',3,3,((#69471,#69472,#69473,#69474,#69475,
#69476,#69477,#69478,#69479,#69480,#69481,#69482,#69483,#69484,#69485,#69486,
#69487,#69488,#69489,#69490,#69491,#69492,#69493,#69494,#69495,#69496,#69497,
#69498,#69499,#69500,#69501,#69502,#69503,#69504,#69505,#69506,#69507,#69508,
#69509,#69510,#69511,#69512,#69513,#69514,#69515,#69516,#69517,#69518,#69519,
#69520,#69521,#69522,#69523,#69524,#69525,#69526,#69527,#69528),(#69529,
#69530,#69531,#69532,#69533,#69534,#69535,#69536,#69537,#69538,#69539,#69540,
#69541,#69542,#69543,#69544,#69545,#69546,#69547,#69548,#69549,#69550,#69551,
#69552,#69553,#69554,#69555,#69556,#69557,#69558,#69559,#69560,#69561,#69562,
#69563,#69564,#69565,#69566,#69567,#69568,#69569,#69570,#69571,#69572,#69573,
#69574,#69575,#69576,#69577,#69578,#69579,#69580,#69581,#69582,#69583,#69584,
#69585,#69586),(#69587,#69588,#69589,#69590,#69591,#69592,#69593,#69594,
#69595,#69596,#69597,#69598,#69599,#69600,#69601,#69602,#69603,#69604,#69605,
#69606,#69607,#69608,#69609,#69610,#69611,#69612,#69613,#69614,#69615,#69616,
#69617,#69618,#69619,#69620,#69621,#69622,#69623,#69624,#69625,#69626,#69627,
#69628,#69629,#69630,#69631,#69632,#69633,#69634,#69635,#69636,#69637,#69638,
#69639,#69640,#69641,#69642,#69643,#69644),(#69645,#69646,#69647,#69648,
#69649,#69650,#69651,#69652,#69653,#69654,#69655,#69656,#69657,#69658,#69659,
#69660,#69661,#69662,#69663,#69664,#69665,#69666,#69667,#69668,#69669,#69670,
#69671,#69672,#69673,#69674,#69675,#69676,#69677,#69678,#69679,#69680,#69681,
#69682,#69683,#69684,#69685,#69686,#69687,#69688,#69689,#69690,#69691,#69692,
#69693,#69694,#69695,#69696,#69697,#69698,#69699,#69700,#69701,#69702)),
 .UNSPECIFIED.,.F.,.F.,.F.,(4,4),(4,1,1,1,1,1,1,1,1,1,1,1,1,1,1,1,1,1,1,
1,1,1,1,1,1,1,1,1,1,1,1,1,1,1,1,1,1,1,1,1,1,1,1,1,1,1,1,1,1,1,1,1,1,1,1,
4),(0.,0.0641840294258107),(11.8589888623078,12.3522141756159,12.8454394889239,
13.8318901155401,14.8183407421562,15.8047913687724,16.7912419953885,17.7776926220047,
18.7641432486208,19.750593875237,20.7370445018531,21.7234951284693,22.7099457550854,
23.6963963817016,24.6828470083177,25.6692976349339,26.65574826155,27.6421988881662,
28.6286495147823,29.6151001413985,30.6015507680146,31.5880013946308,32.5744520212469,
33.5609026478631,34.5473532744792,35.5338039010954,36.5202545277115,37.5067051543277,
38.4931557809438,39.47960640756,40.4660570341761,41.4525076607923,42.4389582874084,
43.4254089140245,44.4118595406407,45.3983101672568,46.384760793873,47.3712114204891,
48.3576620471053,49.3441126737214,50.3305633003376,51.3170139269537,52.3034645535699,
53.289915180186,54.2763658068022,55.2628164334183,56.2492670600345,57.2357176866506,
58.2221683132668,59.2086189398829,60.1950695664991,61.1815201931152,62.1679708197314,
63.1544214463475,63.6476467596556,64.1408720729637),.UNSPECIFIED.);
#359=B_SPLINE_SURFACE_WITH_KNOTS('',3,3,((#69937,#69938,#69939,#69940,#69941,
#69942,#69943,#69944,#69945,#69946,#69947,#69948,#69949,#69950,#69951,#69952,
#69953,#69954,#69955,#69956,#69957,#69958,#69959,#69960,#69961,#69962,#69963,
#69964,#69965,#69966,#69967,#69968,#69969,#69970,#69971,#69972,#69973,#69974,
#69975,#69976,#69977,#69978,#69979,#69980,#69981,#69982,#69983,#69984,#69985,
#69986,#69987,#69988,#69989,#69990,#69991,#69992,#69993,#69994),(#69995,
#69996,#69997,#69998,#69999,#70000,#70001,#70002,#70003,#70004,#70005,#70006,
#70007,#70008,#70009,#70010,#70011,#70012,#70013,#70014,#70015,#70016,#70017,
#70018,#70019,#70020,#70021,#70022,#70023,#70024,#70025,#70026,#70027,#70028,
#70029,#70030,#70031,#70032,#70033,#70034,#70035,#70036,#70037,#70038,#70039,
#70040,#70041,#70042,#70043,#70044,#70045,#70046,#70047,#70048,#70049,#70050,
#70051,#70052),(#70053,#70054,#70055,#70056,#70057,#70058,#70059,#70060,
#70061,#70062,#70063,#70064,#70065,#70066,#70067,#70068,#70069,#70070,#70071,
#70072,#70073,#70074,#70075,#70076,#70077,#70078,#70079,#70080,#70081,#70082,
#70083,#70084,#70085,#70086,#70087,#70088,#70089,#70090,#70091,#70092,#70093,
#70094,#70095,#70096,#70097,#70098,#70099,#70100,#70101,#70102,#70103,#70104,
#70105,#70106,#70107,#70108,#70109,#70110),(#70111,#70112,#70113,#70114,
#70115,#70116,#70117,#70118,#70119,#70120,#70121,#70122,#70123,#70124,#70125,
#70126,#70127,#70128,#70129,#70130,#70131,#70132,#70133,#70134,#70135,#70136,
#70137,#70138,#70139,#70140,#70141,#70142,#70143,#70144,#70145,#70146,#70147,
#70148,#70149,#70150,#70151,#70152,#70153,#70154,#70155,#70156,#70157,#70158,
#70159,#70160,#70161,#70162,#70163,#70164,#70165,#70166,#70167,#70168)),
 .UNSPECIFIED.,.F.,.F.,.F.,(4,4),(4,1,1,1,1,1,1,1,1,1,1,1,1,1,1,1,1,1,1,
1,1,1,1,1,1,1,1,1,1,1,1,1,1,1,1,1,1,1,1,1,1,1,1,1,1,1,1,1,1,1,1,1,1,1,1,
4),(0.,0.0641840294258107),(14.3989442667811,14.8921695800892,15.3853948933972,
16.3718455200134,17.3582961466295,18.3447467732457,19.3311973998618,20.317648026478,
21.3040986530941,22.2905492797103,23.2769999063264,24.2634505329426,25.2499011595587,
26.2363517861749,27.222802412791,28.2092530394072,29.1957036660233,30.1821542926395,
31.1686049192556,32.1550555458718,33.1415061724879,34.1279567991041,35.1144074257202,
36.1008580523364,37.0873086789525,38.0737593055687,39.0602099321848,40.046660558801,
41.0331111854171,42.0195618120333,43.0060124386494,43.9924630652656,44.9789136918817,
45.9653643184979,46.951814945114,47.9382655717301,48.9247161983463,49.9111668249625,
50.8976174515786,51.8840680781948,52.8705187048109,53.856969331427,54.8434199580432,
55.8298705846593,56.8163212112755,57.8027718378916,58.7892224645078,59.7756730911239,
60.7621237177401,61.7485743443562,62.7350249709724,63.7214755975885,64.7079262242047,
65.6943768508208,66.1876021641289,66.680827477437),.UNSPECIFIED.);
#1370=B_SPLINE_CURVE_WITH_KNOTS('',3,(#68897,#68898,#68899,#68900,#68901,
#68902,#68903),.UNSPECIFIED.,.F.,.F.,(4,3,4),(51.5745014586045,51.7886578973478,
52.2818832106559),.UNSPECIFIED.);
#1371=B_SPLINE_CURVE_WITH_KNOTS('',3,(#68906,#68907,#68908,#68909,#68910,
#68911,#68912,#68913,#68914,#68915),.UNSPECIFIED.,.F.,.F.,(4,3,3,4),(-50.2654824574367,
-49.3225313308074,-48.3360807041913,-47.8312715558983),.UNSPECIFIED.);
#1372=B_SPLINE_CURVE_WITH_KNOTS('',3,(#68920,#68921,#68922,#68923,#68924,
#68925,#68926,#68927,#68928,#68929,#68930,#68931,#68932,#68933,#68934,#68935,
#68936,#68937,#68938,#68939,#68940,#68941,#68942,#68943,#68944),
 .UNSPECIFIED.,.F.,.F.,(4,3,3,3,3,3,3,3,4),(45.291316151425,45.3767288243428,
46.363179450959,47.3496300775751,48.3360807041913,49.3225313308074,50.3089819574236,
51.2954325840397,51.5745014586045),.UNSPECIFIED.);
#1373=B_SPLINE_CURVE_WITH_KNOTS('',3,(#68945,#68946,#68947,#68948,#68949,
#68950,#68951,#68952,#68953,#68954,#68955,#68956,#68957,#68958,#68959,#68960,
#68961,#68962,#68963,#68964,#68965,#68966),.UNSPECIFIED.,.F.,.F.,(4,3,3,
3,3,3,3,4),(-47.8312715558983,-47.3496300775751,-46.363179450959,-45.3767288243428,
-44.3902781977267,-43.4038275711106,-42.4173769444944,-41.5480862487187),
 .UNSPECIFIED.);
#1374=B_SPLINE_CURVE_WITH_KNOTS('',3,(#68971,#68972,#68973,#68974,#68975,
#68976,#68977,#68978,#68979,#68980,#68981,#68982,#68983,#68984,#68985,#68986,
#68987,#68988,#68989,#68990,#68991,#68992),.UNSPECIFIED.,.F.,.F.,(4,3,3,
3,3,3,3,4),(39.0081308442454,39.458025064646,40.4444756912621,41.4309263178782,
42.4173769444944,43.4038275711105,44.3902781977267,45.291316151425),
 .UNSPECIFIED.);
#1375=B_SPLINE_CURVE_WITH_KNOTS('',3,(#68993,#68994,#68995,#68996,#68997,
#68998,#68999,#69000,#69001,#69002,#69003,#69004,#69005,#69006,#69007,#69008,
#69009,#69010,#69011,#69012,#69013,#69014,#69015,#69016,#69017),
 .UNSPECIFIED.,.F.,.F.,(4,3,3,3,3,3,3,3,4),(-41.5480862487187,-41.4309263178783,
-40.4444756912621,-39.458025064646,-38.4715744380298,-37.4851238114137,
-36.4986731847975,-35.5122225581814,-35.2649009415391),.UNSPECIFIED.);
#1376=B_SPLINE_CURVE_WITH_KNOTS('',3,(#69022,#69023,#69024,#69025,#69026,
#69027,#69028,#69029,#69030,#69031,#69032,#69033,#69034,#69035,#69036,#69037,
#69038,#69039,#69040,#69041,#69042,#69043),.UNSPECIFIED.,.F.,.F.,(4,3,3,
3,3,3,3,4),(32.7249455370658,33.5393213049491,34.5257719315652,35.5122225581814,
36.4986731847975,37.4851238114137,38.4715744380298,39.0081308442454),
 .UNSPECIFIED.);
#1377=B_SPLINE_CURVE_WITH_KNOTS('',3,(#69044,#69045,#69046,#69047,#69048,
#69049,#69050,#69051,#69052,#69053,#69054,#69055,#69056,#69057,#69058,#69059,
#69060,#69061,#69062,#69063,#69064,#69065),.UNSPECIFIED.,.F.,.F.,(4,3,3,
3,3,3,3,4),(-35.2649009415391,-34.5257719315652,-33.5393213049491,-32.5528706783329,
-31.5664200517168,-30.5799694251006,-29.5935187984845,-28.9817156343595),
 .UNSPECIFIED.);
#1378=B_SPLINE_CURVE_WITH_KNOTS('',3,(#69070,#69071,#69072,#69073,#69074,
#69075,#69076,#69077,#69078,#69079,#69080,#69081,#69082,#69083,#69084,#69085,
#69086,#69087,#69088,#69089,#69090,#69091,#69092,#69093,#69094),
 .UNSPECIFIED.,.F.,.F.,(4,3,3,3,3,3,3,3,4),(26.4417602298862,26.634166918636,
27.6206175452522,28.6070681718683,29.5935187984845,30.5799694251006,31.5664200517168,
32.5528706783329,32.7249455370658),.UNSPECIFIED.);
#1379=B_SPLINE_CURVE_WITH_KNOTS('',3,(#69095,#69096,#69097,#69098,#69099,
#69100,#69101,#69102,#69103,#69104,#69105,#69106,#69107,#69108,#69109,#69110,
#69111,#69112,#69113,#69114,#69115,#69116),.UNSPECIFIED.,.F.,.F.,(4,3,3,
3,3,3,3,4),(-28.9817156343595,-28.6070681718683,-27.6206175452522,-26.634166918636,
-25.6477162920199,-24.6612656654037,-23.6748150387876,-22.6985303271799),
 .UNSPECIFIED.);
#1380=B_SPLINE_CURVE_WITH_KNOTS('',3,(#69121,#69122,#69123,#69124,#69125,
#69126,#69127,#69128,#69129,#69130,#69131,#69132,#69133,#69134,#69135,#69136,
#69137,#69138,#69139,#69140,#69141,#69142),.UNSPECIFIED.,.F.,.F.,(4,3,3,
3,3,3,3,4),(20.1585749227066,20.7154631589391,21.7019137855553,22.6883644121714,
23.6748150387876,24.6612656654037,25.6477162920199,26.4417602298862),
 .UNSPECIFIED.);
#1381=B_SPLINE_CURVE_WITH_KNOTS('',3,(#69143,#69144,#69145,#69146,#69147,
#69148,#69149,#69150,#69151,#69152,#69153,#69154,#69155,#69156,#69157,#69158,
#69159,#69160,#69161,#69162,#69163,#69164,#69165,#69166,#69167),
 .UNSPECIFIED.,.F.,.F.,(4,3,3,3,3,3,3,3,4),(-22.6985303271799,-22.6883644121714,
-21.7019137855553,-20.7154631589391,-19.729012532323,-18.7425619057068,
-17.7561112790907,-16.7696606524745,-16.4153450200003),.UNSPECIFIED.);
#1382=B_SPLINE_CURVE_WITH_KNOTS('',3,(#69172,#69173,#69174,#69175,#69176,
#69177,#69178,#69179,#69180,#69181,#69182,#69183,#69184,#69185,#69186,#69187,
#69188,#69189,#69190,#69191,#69192,#69193),.UNSPECIFIED.,.F.,.F.,(4,3,3,
3,3,3,3,4),(13.875389615527,14.7967593992422,15.7832100258584,16.7696606524745,
17.7561112790907,18.7425619057068,19.729012532323,20.1585749227066),
 .UNSPECIFIED.);
#1383=B_SPLINE_CURVE_WITH_KNOTS('',3,(#69194,#69195,#69196,#69197,#69198,
#69199,#69200,#69201,#69202,#69203,#69204,#69205,#69206,#69207,#69208,#69209,
#69210,#69211,#69212,#69213,#69214,#69215),.UNSPECIFIED.,.F.,.F.,(4,3,3,
3,3,3,3,4),(-16.4153450200003,-15.7832100258584,-14.7967593992422,-13.8103087726261,
-12.8238581460099,-11.8374075193938,-10.8509568927776,-10.1321597128207),
 .UNSPECIFIED.);
#1384=B_SPLINE_CURVE_WITH_KNOTS('',3,(#69221,#69222,#69223,#69224,#69225,
#69226,#69227,#69228,#69229,#69230,#69231,#69232,#69233,#69234,#69235,#69236),
 .UNSPECIFIED.,.F.,.F.,(4,3,3,3,3,4),(-3.84897440564117,-2.95935187984845,
-1.9729012532323,-0.986450626616147,-0.493225313308074,0.),
 .UNSPECIFIED.);
#1385=B_SPLINE_CURVE_WITH_KNOTS('',3,(#69239,#69240,#69241,#69242,#69243,
#69244,#69245,#69246,#69247,#69248,#69249,#69250,#69251,#69252,#69253,#69254,
#69255,#69256,#69257),.UNSPECIFIED.,.F.,.F.,(4,3,3,3,3,3,4),(2.01640075321919,
2.95935187984845,3.9458025064646,4.93225313308074,5.9187037596969,6.90515438631305,
7.59220430834742),.UNSPECIFIED.);
#1386=B_SPLINE_CURVE_WITH_KNOTS('',3,(#69263,#69264,#69265,#69266,#69267,
#69268,#69269,#69270,#69271),.UNSPECIFIED.,.F.,.F.,(4,1,1,1,1,1,4),(59.6902604182061,
60.1950695664991,61.1815201931152,62.1679708197314,63.1544214463475,63.6476467596556,
64.1408720729637),.UNSPECIFIED.);
#1387=B_SPLINE_CURVE_WITH_KNOTS('',3,(#69274,#69275,#69276,#69277,#69278,
#69279,#69280,#69281,#69282),.UNSPECIFIED.,.F.,.F.,(4,1,1,1,1,1,4),(59.6902604182061,
59.7756730911239,60.7621237177401,61.7485743443562,62.7350249709724,63.7214755975885,
64.6644267242178),.UNSPECIFIED.);
#1388=B_SPLINE_CURVE_WITH_KNOTS('',3,(#69287,#69288,#69289,#69290,#69291,
#69292,#69293,#69294,#69295,#69296),.UNSPECIFIED.,.F.,.F.,(4,1,1,1,1,1,
1,4),(53.4070751110265,54.2763658068022,55.2628164334183,56.2492670600345,
57.2357176866506,58.2221683132668,59.2086189398829,59.6902604182061),
 .UNSPECIFIED.);
#1389=B_SPLINE_CURVE_WITH_KNOTS('',3,(#69297,#69298,#69299,#69300,#69301,
#69302,#69303,#69304,#69305,#69306),.UNSPECIFIED.,.F.,.F.,(4,1,1,1,1,1,
1,4),(53.4070751110265,53.856969331427,54.8434199580432,55.8298705846593,
56.8163212112755,57.8027718378916,58.7892224645078,59.6902604182061),
 .UNSPECIFIED.);
#1390=B_SPLINE_CURVE_WITH_KNOTS('',3,(#69311,#69312,#69313,#69314,#69315,
#69316,#69317,#69318,#69319,#69320,#69321),.UNSPECIFIED.,.F.,.F.,(4,1,1,
1,1,1,1,1,4),(47.1238898038469,47.3712114204891,48.3576620471053,49.3441126737214,
50.3305633003376,51.3170139269537,52.3034645535699,53.289915180186,53.4070751110265),
 .UNSPECIFIED.);
#1391=B_SPLINE_CURVE_WITH_KNOTS('',3,(#69322,#69323,#69324,#69325,#69326,
#69327,#69328,#69329,#69330,#69331),.UNSPECIFIED.,.F.,.F.,(4,1,1,1,1,1,
1,4),(47.1238898038469,47.9382655717301,48.9247161983463,49.9111668249625,
50.8976174515786,51.8840680781948,52.8705187048109,53.4070751110265),
 .UNSPECIFIED.);
#1392=B_SPLINE_CURVE_WITH_KNOTS('',3,(#69336,#69337,#69338,#69339,#69340,
#69341,#69342,#69343,#69344,#69345),.UNSPECIFIED.,.F.,.F.,(4,1,1,1,1,1,
1,4),(40.8407044966673,41.4525076607923,42.4389582874084,43.4254089140245,
44.4118595406407,45.3983101672568,46.384760793873,47.1238898038469),
 .UNSPECIFIED.);
#1393=B_SPLINE_CURVE_WITH_KNOTS('',3,(#69346,#69347,#69348,#69349,#69350,
#69351,#69352,#69353,#69354,#69355,#69356),.UNSPECIFIED.,.F.,.F.,(4,1,1,
1,1,1,1,1,4),(40.8407044966673,41.0331111854171,42.0195618120333,43.0060124386494,
43.9924630652656,44.9789136918817,45.9653643184979,46.951814945114,47.1238898038469),
 .UNSPECIFIED.);
#1394=B_SPLINE_CURVE_WITH_KNOTS('',3,(#69361,#69362,#69363,#69364,#69365,
#69366,#69367,#69368,#69369,#69370),.UNSPECIFIED.,.F.,.F.,(4,1,1,1,1,1,
1,4),(34.5575191894877,35.5338039010954,36.5202545277115,37.5067051543277,
38.4931557809438,39.47960640756,40.4660570341761,40.8407044966673),
 .UNSPECIFIED.);
#1395=B_SPLINE_CURVE_WITH_KNOTS('',3,(#69371,#69372,#69373,#69374,#69375,
#69376,#69377,#69378,#69379,#69380),.UNSPECIFIED.,.F.,.F.,(4,1,1,1,1,1,
1,4),(34.5575191894877,35.1144074257202,36.1008580523364,37.0873086789525,
38.0737593055687,39.0602099321848,40.046660558801,40.8407044966673),
 .UNSPECIFIED.);
#1396=B_SPLINE_CURVE_WITH_KNOTS('',3,(#69385,#69386,#69387,#69388,#69389,
#69390,#69391,#69392,#69393,#69394,#69395),.UNSPECIFIED.,.F.,.F.,(4,1,1,
1,1,1,1,1,4),(28.2743338823081,28.6286495147823,29.6151001413985,30.6015507680146,
31.5880013946308,32.5744520212469,33.5609026478631,34.5473532744792,34.5575191894877),
 .UNSPECIFIED.);
#1397=B_SPLINE_CURVE_WITH_KNOTS('',3,(#69396,#69397,#69398,#69399,#69400,
#69401,#69402,#69403,#69404,#69405),.UNSPECIFIED.,.F.,.F.,(4,1,1,1,1,1,
1,4),(28.2743338823081,29.1957036660233,30.1821542926395,31.1686049192556,
32.1550555458718,33.1415061724879,34.1279567991041,34.5575191894877),
 .UNSPECIFIED.);
#1398=B_SPLINE_CURVE_WITH_KNOTS('',3,(#69410,#69411,#69412,#69413,#69414,
#69415,#69416,#69417,#69418,#69419),.UNSPECIFIED.,.F.,.F.,(4,1,1,1,1,1,
1,4),(21.9911485751285,22.7099457550854,23.6963963817016,24.6828470083177,
25.6692976349339,26.65574826155,27.6421988881662,28.2743338823081),
 .UNSPECIFIED.);
#1399=B_SPLINE_CURVE_WITH_KNOTS('',3,(#69420,#69421,#69422,#69423,#69424,
#69425,#69426,#69427,#69428,#69429,#69430),.UNSPECIFIED.,.F.,.F.,(4,1,1,
1,1,1,1,1,4),(21.9911485751285,22.2905492797103,23.2769999063264,24.2634505329426,
25.2499011595587,26.2363517861749,27.222802412791,28.2092530394072,28.2743338823081),
 .UNSPECIFIED.);
#1400=B_SPLINE_CURVE_WITH_KNOTS('',3,(#69436,#69437,#69438,#69439,#69440,
#69441),.UNSPECIFIED.,.F.,.F.,(4,1,1,4),(14.3989442667811,14.8921695800892,
15.3853948933972,15.7079632679489),.UNSPECIFIED.);
#1401=B_SPLINE_CURVE_WITH_KNOTS('',3,(#69444,#69445,#69446,#69447,#69448),
 .UNSPECIFIED.,.F.,.F.,(4,1,4),(13.875389615527,14.8183407421562,15.7079632679489),
 .UNSPECIFIED.);
#1402=B_SPLINE_CURVE_WITH_KNOTS('',3,(#69450,#69451,#69452,#69453,#69454,
#69455,#69456,#69457,#69458,#69459,#69460),.UNSPECIFIED.,.F.,.F.,(4,1,1,
1,1,1,1,1,4),(15.7079632679489,15.8047913687724,16.7912419953885,17.7776926220047,
18.7641432486208,19.750593875237,20.7370445018531,21.7234951284693,21.9911485751285),
 .UNSPECIFIED.);
#1403=B_SPLINE_CURVE_WITH_KNOTS('',3,(#69461,#69462,#69463,#69464,#69465,
#69466,#69467,#69468,#69469,#69470),.UNSPECIFIED.,.F.,.F.,(4,1,1,1,1,1,
1,4),(15.7079632679489,16.3718455200134,17.3582961466295,18.3447467732457,
19.3311973998618,20.317648026478,21.3040986530941,21.9911485751285),
 .UNSPECIFIED.);
#1404=B_SPLINE_CURVE_WITH_KNOTS('',3,(#69703,#69704,#69705,#69706,#69707,
#69708,#69709,#69710,#69711,#69712,#69713,#69714,#69715,#69716,#69717,#69718,
#69719,#69720,#69721,#69722,#69723,#69724,#69725,#69726,#69727,#69728,#69729,
#69730,#69731,#69732,#69733,#69734,#69735,#69736,#69737,#69738,#69739,#69740,
#69741,#69742,#69743,#69744,#69745,#69746,#69747,#69748,#69749,#69750,#69751,
#69752,#69753,#69754,#69755,#69756,#69757,#69758,#69759,#69760,#69761,#69762,
#69763,#69764,#69765,#69766,#69767,#69768,#69769,#69770,#69771,#69772,#69773,
#69774,#69775,#69776,#69777,#69778,#69779,#69780,#69781,#69782,#69783,#69784,
#69785,#69786,#69787,#69788,#69789,#69790,#69791,#69792,#69793,#69794,#69795,
#69796,#69797,#69798,#69799,#69800,#69801,#69802,#69803,#69804,#69805,#69806,
#69807,#69808),.UNSPECIFIED.,.F.,.F.,(4,3,3,3,3,3,3,3,3,3,3,3,3,3,3,3,3,
3,3,3,3,3,3,3,3,3,3,3,3,3,3,3,3,3,3,4),(0.,0.0439873495596682,0.088535234885729,
0.133203648537345,0.177539443303643,0.193269018030229,0.199971189808446,
0.243934275067846,0.248071778815114,0.292055723719706,0.335717872507241,
0.374210944067843,0.384315712222397,0.391619070879034,0.434698852730331,
0.47712046629841,0.48969015874965,0.533088907914198,0.559308924386188,0.574291000021554,
0.57984588764462,0.62205897872085,0.66496509314549,0.707636118884185,0.738257750456918,
0.752576412624451,0.758605909671541,0.765028679465915,0.807111218921827,
0.843485707057882,0.85917048475052,0.866049641644265,0.873236607794053,
0.913787166992983,0.952609171466047,0.972375876542335),.UNSPECIFIED.);
#1405=B_SPLINE_CURVE_WITH_KNOTS('',3,(#69809,#69810,#69811,#69812,#69813,
#69814,#69815,#69816,#69817,#69818,#69819,#69820,#69821,#69822,#69823,#69824,
#69825,#69826,#69827,#69828,#69829,#69830,#69831,#69832,#69833,#69834,#69835,
#69836,#69837,#69838,#69839,#69840,#69841,#69842,#69843,#69844,#69845,#69846,
#69847,#69848,#69849,#69850,#69851,#69852,#69853,#69854,#69855,#69856,#69857,
#69858,#69859,#69860,#69861,#69862,#69863,#69864,#69865,#69866,#69867,#69868,
#69869,#69870,#69871,#69872,#69873,#69874,#69875,#69876,#69877,#69878,#69879,
#69880,#69881,#69882,#69883,#69884,#69885,#69886,#69887,#69888,#69889,#69890,
#69891,#69892,#69893,#69894,#69895,#69896,#69897,#69898,#69899,#69900,#69901,
#69902,#69903,#69904,#69905,#69906,#69907,#69908,#69909,#69910,#69911),
 .UNSPECIFIED.,.F.,.F.,(4,3,3,3,3,3,3,3,3,3,3,3,3,3,3,3,3,3,3,3,3,3,3,3,
3,3,3,3,3,3,3,3,3,3,4),(0.,0.0403422905180338,0.0813682734786595,0.122949980351713,
0.16449095941097,0.178014361827899,0.183409369411602,0.227186329885339,
0.269229509469957,0.311535350955759,0.348916065443153,0.357705618004978,
0.364415764229672,0.407315005273426,0.450191512111689,0.461058208905336,
0.503507289353387,0.531285871131442,0.541027225498738,0.546474827271459,
0.552442453195144,0.594916660917874,0.639047653028424,0.683117962531696,
0.716223791940519,0.731747366121405,0.738184546707727,0.782779716156374,
0.824075936567849,0.84301368069624,0.852796512264844,0.860145827789084,
0.904729831180339,0.947964597802275,0.97000658757344),.UNSPECIFIED.);
#1406=B_SPLINE_CURVE_WITH_KNOTS('',3,(#69912,#69913,#69914,#69915,#69916,
#69917,#69918,#69919,#69920,#69921,#69922,#69923,#69924,#69925,#69926,#69927,
#69928,#69929,#69930,#69931,#69932,#69933,#69934,#69935,#69936),
 .UNSPECIFIED.,.F.,.F.,(4,3,3,3,3,3,3,3,4),(-10.1321597128207,-9.86450626616149,
-8.87805563954534,-7.89160501292919,-6.90515438631305,-5.91870375969689,
-4.93225313308075,-3.94580250646459,-3.84897440564117),.UNSPECIFIED.);
#1407=B_SPLINE_CURVE_WITH_KNOTS('',3,(#70169,#70170,#70171,#70172,#70173,
#70174,#70175,#70176,#70177,#70178,#70179,#70180,#70181,#70182,#70183,#70184,
#70185,#70186,#70187,#70188,#70189,#70190,#70191,#70192,#70193,#70194,#70195,
#70196,#70197,#70198,#70199,#70200,#70201,#70202,#70203,#70204,#70205,#70206,
#70207,#70208,#70209,#70210,#70211,#70212,#70213,#70214,#70215,#70216,#70217,
#70218,#70219,#70220,#70221,#70222,#70223,#70224,#70225,#70226,#70227,#70228,
#70229,#70230,#70231,#70232,#70233,#70234,#70235,#70236,#70237,#70238,#70239,
#70240,#70241,#70242,#70243,#70244,#70245,#70246,#70247,#70248,#70249,#70250,
#70251,#70252,#70253,#70254,#70255,#70256,#70257,#70258,#70259,#70260,#70261,
#70262,#70263,#70264,#70265,#70266,#70267,#70268,#70269,#70270,#70271),
 .UNSPECIFIED.,.F.,.F.,(4,3,3,3,3,3,3,3,3,3,3,3,3,3,3,3,3,3,3,3,3,3,3,3,
3,3,3,3,3,3,3,3,3,3,4),(0.,0.0403420728543006,0.0813678367855401,0.122949539928715,
0.164490759249614,0.178014431809021,0.183409385478703,0.227186329885338,
0.269229949539637,0.311536068831159,0.348916603849705,0.357706091108837,
0.364415856383174,0.407315466341614,0.450192046682075,0.461058208905346,
0.5035070595844,0.531285655723017,0.541026743529684,0.54647402973548,0.552442268108838,
0.59491621056702,0.639047258971427,0.683117463220518,0.716223355043237,
0.731746708435023,0.738183753475272,0.782778798969233,0.824075248677492,
0.843013807341498,0.852796973522259,0.860145921094186,0.904729940902664,
0.947964597802271,0.970006587573432),.UNSPECIFIED.);
#1408=B_SPLINE_CURVE_WITH_KNOTS('',3,(#70272,#70273,#70274,#70275,#70276,
#70277,#70278,#70279,#70280,#70281,#70282,#70283,#70284,#70285,#70286,#70287,
#70288,#70289,#70290,#70291,#70292,#70293,#70294,#70295,#70296),
 .UNSPECIFIED.,.F.,.F.,(4,3,3,3,3,3,3,3,4),(7.59220430834742,7.89160501292919,
8.87805563954534,9.86450626616149,10.8509568927776,11.8374075193938,12.8238581460099,
13.8103087726261,13.875389615527),.UNSPECIFIED.);
#1409=B_SPLINE_CURVE_WITH_KNOTS('',3,(#70297,#70298,#70299,#70300,#70301,
#70302,#70303,#70304,#70305,#70306,#70307,#70308,#70309,#70310,#70311,#70312,
#70313,#70314,#70315,#70316,#70317,#70318,#70319,#70320,#70321,#70322,#70323,
#70324,#70325,#70326,#70327,#70328,#70329,#70330,#70331,#70332,#70333,#70334,
#70335,#70336,#70337,#70338,#70339,#70340,#70341,#70342,#70343,#70344,#70345,
#70346,#70347,#70348,#70349,#70350,#70351,#70352,#70353,#70354,#70355,#70356,
#70357,#70358,#70359,#70360,#70361,#70362,#70363,#70364,#70365,#70366,#70367,
#70368,#70369,#70370,#70371,#70372,#70373,#70374,#70375,#70376,#70377,#70378,
#70379,#70380,#70381,#70382,#70383,#70384,#70385,#70386,#70387,#70388,#70389,
#70390,#70391,#70392,#70393,#70394,#70395,#70396,#70397,#70398,#70399,#70400,
#70401,#70402),.UNSPECIFIED.,.F.,.F.,(4,3,3,3,3,3,3,3,3,3,3,3,3,3,3,3,3,
3,3,3,3,3,3,3,3,3,3,3,3,3,3,3,3,3,3,4),(0.,0.0439870213484189,0.0885347768590274,
0.133203573182163,0.177540067473735,0.193271868519026,0.199972102087808,
0.24393536506854,0.248071778815114,0.29205601261511,0.335718137618304,0.374211142901135,
0.3843154671772,0.391619008898289,0.434698890696845,0.477120259746675,0.489690158749629,
0.533088750991939,0.55930877727157,0.574290713387234,0.579845401630218,
0.622058272372198,0.664964305291723,0.707635330968564,0.738257061030748,
0.752575428668685,0.758604644157454,0.765028377494937,0.80711091192384,
0.843485476809388,0.85917031769407,0.86604942682694,0.87323655891021,0.913787164180478,
0.95260917146603,0.972375876542318),.UNSPECIFIED.);
#2224=SHAPE_REPRESENTATION_RELATIONSHIP('SRR','None',#97618,#2243);
#2243=ADVANCED_BREP_SHAPE_REPRESENTATION('',(#2281),#97468);
#2262=STYLED_ITEM('',(#97722),#2281);
#2281=MANIFOLD_SOLID_BREP('Body1',#21823);
#2355=FACE_BOUND('',#4462,.T.);
#2356=FACE_BOUND('',#4471,.T.);
#2497=PLANE('',#22972);
#2498=PLANE('',#22974);
#2499=PLANE('',#22975);
#2500=PLANE('',#22976);
#2501=PLANE('',#22977);
#2502=PLANE('',#22978);
#2503=PLANE('',#22979);
#2504=PLANE('',#22980);
#3221=FACE_OUTER_BOUND('',#4442,.T.);
#3222=FACE_OUTER_BOUND('',#4443,.T.);
#3223=FACE_OUTER_BOUND('',#4444,.T.);
#3224=FACE_OUTER_BOUND('',#4445,.T.);
#3225=FACE_OUTER_BOUND('',#4446,.T.);
#3226=FACE_OUTER_BOUND('',#4447,.T.);
#3227=FACE_OUTER_BOUND('',#4448,.T.);
#3228=FACE_OUTER_BOUND('',#4449,.T.);
#3229=FACE_OUTER_BOUND('',#4450,.T.);
#3230=FACE_OUTER_BOUND('',#4451,.T.);
#3231=FACE_OUTER_BOUND('',#4452,.T.);
#3232=FACE_OUTER_BOUND('',#4453,.T.);
#3233=FACE_OUTER_BOUND('',#4454,.T.);
#3234=FACE_OUTER_BOUND('',#4455,.T.);
#3235=FACE_OUTER_BOUND('',#4456,.T.);
#3236=FACE_OUTER_BOUND('',#4457,.T.);
#3237=FACE_OUTER_BOUND('',#4458,.T.);
#3238=FACE_OUTER_BOUND('',#4459,.T.);
#3239=FACE_OUTER_BOUND('',#4460,.T.);
#3240=FACE_OUTER_BOUND('',#4461,.T.);
#3241=FACE_OUTER_BOUND('',#4463,.T.);
#3242=FACE_OUTER_BOUND('',#4464,.T.);
#3243=FACE_OUTER_BOUND('',#4465,.T.);
#3244=FACE_OUTER_BOUND('',#4466,.T.);
#3245=FACE_OUTER_BOUND('',#4467,.T.);
#3246=FACE_OUTER_BOUND('',#4468,.T.);
#3247=FACE_OUTER_BOUND('',#4469,.T.);
#3248=FACE_OUTER_BOUND('',#4470,.T.);
#4442=EDGE_LOOP('',(#16998,#16999,#17000,#17001));
#4443=EDGE_LOOP('',(#17002,#17003,#17004,#17005));
#4444=EDGE_LOOP('',(#17006,#17007,#17008,#17009));
#4445=EDGE_LOOP('',(#17010,#17011,#17012,#17013));
#4446=EDGE_LOOP('',(#17014,#17015,#17016,#17017));
#4447=EDGE_LOOP('',(#17018,#17019,#17020,#17021));
#4448=EDGE_LOOP('',(#17022,#17023,#17024,#17025));
#4449=EDGE_LOOP('',(#17026,#17027,#17028,#17029));
#4450=EDGE_LOOP('',(#17030,#17031,#17032,#17033));
#4451=EDGE_LOOP('',(#17034,#17035,#17036,#17037));
#4452=EDGE_LOOP('',(#17038,#17039,#17040,#17041));
#4453=EDGE_LOOP('',(#17042,#17043,#17044,#17045));
#4454=EDGE_LOOP('',(#17046,#17047,#17048,#17049));
#4455=EDGE_LOOP('',(#17050,#17051,#17052,#17053));
#4456=EDGE_LOOP('',(#17054,#17055,#17056,#17057));
#4457=EDGE_LOOP('',(#17058,#17059,#17060,#17061));
#4458=EDGE_LOOP('',(#17062,#17063,#17064,#17065));
#4459=EDGE_LOOP('',(#17066,#17067,#17068,#17069,#17070,#17071,#17072,#17073,
#17074,#17075,#17076,#17077,#17078,#17079,#17080,#17081,#17082,#17083,#17084,
#17085));
#4460=EDGE_LOOP('',(#17086,#17087,#17088,#17089,#17090,#17091,#17092,#17093,
#17094,#17095,#17096,#17097,#17098,#17099,#17100,#17101,#17102,#17103,#17104,
#17105));
#4461=EDGE_LOOP('',(#17106,#17107,#17108,#17109,#17110,#17111));
#4462=EDGE_LOOP('',(#17112,#17113,#17114,#17115));
#4463=EDGE_LOOP('',(#17116,#17117,#17118,#17119));
#4464=EDGE_LOOP('',(#17120,#17121,#17122,#17123));
#4465=EDGE_LOOP('',(#17124,#17125,#17126,#17127));
#4466=EDGE_LOOP('',(#17128,#17129,#17130,#17131));
#4467=EDGE_LOOP('',(#17132,#17133,#17134,#17135));
#4468=EDGE_LOOP('',(#17136,#17137,#17138,#17139));
#4469=EDGE_LOOP('',(#17140,#17141,#17142,#17143));
#4470=EDGE_LOOP('',(#17144,#17145,#17146,#17147,#17148,#17149));
#4471=EDGE_LOOP('',(#17150,#17151,#17152,#17153));
#5690=LINE('',#68895,#6904);
#5691=LINE('',#68919,#6905);
#5692=LINE('',#68970,#6906);
#5693=LINE('',#69021,#6907);
#5694=LINE('',#69069,#6908);
#5695=LINE('',#69120,#6909);
#5696=LINE('',#69171,#6910);
#5697=LINE('',#69219,#6911);
#5698=LINE('',#69261,#6912);
#5699=LINE('',#69286,#6913);
#5700=LINE('',#69310,#6914);
#5701=LINE('',#69335,#6915);
#5702=LINE('',#69360,#6916);
#5703=LINE('',#69384,#6917);
#5704=LINE('',#69409,#6918);
#5705=LINE('',#69434,#6919);
#5706=LINE('',#70406,#6920);
#5707=LINE('',#70408,#6921);
#5708=LINE('',#70410,#6922);
#5709=LINE('',#70412,#6923);
#5710=LINE('',#70414,#6924);
#5711=LINE('',#70415,#6925);
#5712=LINE('',#70420,#6926);
#5713=LINE('',#70421,#6927);
#5714=LINE('',#70422,#6928);
#5715=LINE('',#70425,#6929);
#5716=LINE('',#70426,#6930);
#5717=LINE('',#70429,#6931);
#5718=LINE('',#70430,#6932);
#5719=LINE('',#70433,#6933);
#5720=LINE('',#70434,#6934);
#5721=LINE('',#70437,#6935);
#5722=LINE('',#70438,#6936);
#5723=LINE('',#70440,#6937);
#6904=VECTOR('',#26080,5.);
#6905=VECTOR('',#26085,5.);
#6906=VECTOR('',#26088,5.);
#6907=VECTOR('',#26091,5.);
#6908=VECTOR('',#26094,5.);
#6909=VECTOR('',#26097,5.);
#6910=VECTOR('',#26100,5.);
#6911=VECTOR('',#26103,5.);
#6912=VECTOR('',#26108,5.0736);
#6913=VECTOR('',#26113,5.0736);
#6914=VECTOR('',#26116,5.0736);
#6915=VECTOR('',#26119,5.0736);
#6916=VECTOR('',#26122,5.0736);
#6917=VECTOR('',#26125,5.0736);
#6918=VECTOR('',#26128,5.0736);
#6919=VECTOR('',#26131,5.0736);
#6920=VECTOR('',#26138,10.);
#6921=VECTOR('',#26139,10.);
#6922=VECTOR('',#26140,10.);
#6923=VECTOR('',#26141,10.);
#6924=VECTOR('',#26142,10.);
#6925=VECTOR('',#26143,10.);
#6926=VECTOR('',#26148,10.);
#6927=VECTOR('',#26149,10.);
#6928=VECTOR('',#26150,10.);
#6929=VECTOR('',#26153,10.);
#6930=VECTOR('',#26154,10.);
#6931=VECTOR('',#26157,10.);
#6932=VECTOR('',#26158,10.);
#6933=VECTOR('',#26161,10.);
#6934=VECTOR('',#26162,10.);
#6935=VECTOR('',#26165,10.);
#6936=VECTOR('',#26166,10.);
#6937=VECTOR('',#26169,10.);
#7559=CIRCLE('',#22952,4.51775);
#7560=CIRCLE('',#22960,4.51775);
#7561=CIRCLE('',#22962,5.0736);
#7562=CIRCLE('',#22970,5.0736);
#8909=VERTEX_POINT('',#68893);
#8910=VERTEX_POINT('',#68894);
#8911=VERTEX_POINT('',#68896);
#8912=VERTEX_POINT('',#68904);
#8913=VERTEX_POINT('',#68917);
#8914=VERTEX_POINT('',#68918);
#8915=VERTEX_POINT('',#68968);
#8916=VERTEX_POINT('',#68969);
#8917=VERTEX_POINT('',#69019);
#8918=VERTEX_POINT('',#69020);
#8919=VERTEX_POINT('',#69067);
#8920=VERTEX_POINT('',#69068);
#8921=VERTEX_POINT('',#69118);
#8922=VERTEX_POINT('',#69119);
#8923=VERTEX_POINT('',#69169);
#8924=VERTEX_POINT('',#69170);
#8925=VERTEX_POINT('',#69217);
#8926=VERTEX_POINT('',#69218);
#8927=VERTEX_POINT('',#69220);
#8928=VERTEX_POINT('',#69237);
#8929=VERTEX_POINT('',#69259);
#8930=VERTEX_POINT('',#69260);
#8931=VERTEX_POINT('',#69262);
#8932=VERTEX_POINT('',#69272);
#8933=VERTEX_POINT('',#69284);
#8934=VERTEX_POINT('',#69285);
#8935=VERTEX_POINT('',#69308);
#8936=VERTEX_POINT('',#69309);
#8937=VERTEX_POINT('',#69333);
#8938=VERTEX_POINT('',#69334);
#8939=VERTEX_POINT('',#69358);
#8940=VERTEX_POINT('',#69359);
#8941=VERTEX_POINT('',#69382);
#8942=VERTEX_POINT('',#69383);
#8943=VERTEX_POINT('',#69407);
#8944=VERTEX_POINT('',#69408);
#8945=VERTEX_POINT('',#69432);
#8946=VERTEX_POINT('',#69433);
#8947=VERTEX_POINT('',#69435);
#8948=VERTEX_POINT('',#69442);
#8949=VERTEX_POINT('',#70404);
#8950=VERTEX_POINT('',#70405);
#8951=VERTEX_POINT('',#70407);
#8952=VERTEX_POINT('',#70409);
#8953=VERTEX_POINT('',#70411);
#8954=VERTEX_POINT('',#70413);
#8955=VERTEX_POINT('',#70418);
#8956=VERTEX_POINT('',#70419);
#8957=VERTEX_POINT('',#70424);
#8958=VERTEX_POINT('',#70428);
#8959=VERTEX_POINT('',#70432);
#8960=VERTEX_POINT('',#70436);
#11756=EDGE_CURVE('',#8909,#8910,#5690,.T.);
#11757=EDGE_CURVE('',#8910,#8911,#1370,.T.);
#11758=EDGE_CURVE('',#8912,#8911,#7559,.F.);
#11759=EDGE_CURVE('',#8912,#8909,#1371,.T.);
#11760=EDGE_CURVE('',#8913,#8914,#5691,.T.);
#11761=EDGE_CURVE('',#8914,#8910,#1372,.T.);
#11762=EDGE_CURVE('',#8909,#8913,#1373,.T.);
#11763=EDGE_CURVE('',#8915,#8916,#5692,.T.);
#11764=EDGE_CURVE('',#8916,#8914,#1374,.T.);
#11765=EDGE_CURVE('',#8913,#8915,#1375,.T.);
#11766=EDGE_CURVE('',#8917,#8918,#5693,.T.);
#11767=EDGE_CURVE('',#8918,#8916,#1376,.T.);
#11768=EDGE_CURVE('',#8915,#8917,#1377,.T.);
#11769=EDGE_CURVE('',#8919,#8920,#5694,.T.);
#11770=EDGE_CURVE('',#8920,#8918,#1378,.T.);
#11771=EDGE_CURVE('',#8917,#8919,#1379,.T.);
#11772=EDGE_CURVE('',#8921,#8922,#5695,.T.);
#11773=EDGE_CURVE('',#8922,#8920,#1380,.T.);
#11774=EDGE_CURVE('',#8919,#8921,#1381,.T.);
#11775=EDGE_CURVE('',#8923,#8924,#5696,.T.);
#11776=EDGE_CURVE('',#8924,#8922,#1382,.T.);
#11777=EDGE_CURVE('',#8921,#8923,#1383,.T.);
#11778=EDGE_CURVE('',#8925,#8926,#5697,.T.);
#11779=EDGE_CURVE('',#8925,#8927,#1384,.T.);
#11780=EDGE_CURVE('',#8928,#8927,#7560,.T.);
#11781=EDGE_CURVE('',#8928,#8926,#1385,.T.);
#11782=EDGE_CURVE('',#8929,#8930,#5698,.T.);
#11783=EDGE_CURVE('',#8930,#8931,#1386,.T.);
#11784=EDGE_CURVE('',#8932,#8931,#7561,.T.);
#11785=EDGE_CURVE('',#8929,#8932,#1387,.T.);
#11786=EDGE_CURVE('',#8933,#8934,#5699,.T.);
#11787=EDGE_CURVE('',#8934,#8930,#1388,.T.);
#11788=EDGE_CURVE('',#8933,#8929,#1389,.T.);
#11789=EDGE_CURVE('',#8935,#8936,#5700,.T.);
#11790=EDGE_CURVE('',#8936,#8934,#1390,.T.);
#11791=EDGE_CURVE('',#8935,#8933,#1391,.T.);
#11792=EDGE_CURVE('',#8937,#8938,#5701,.T.);
#11793=EDGE_CURVE('',#8938,#8936,#1392,.T.);
#11794=EDGE_CURVE('',#8937,#8935,#1393,.T.);
#11795=EDGE_CURVE('',#8939,#8940,#5702,.T.);
#11796=EDGE_CURVE('',#8940,#8938,#1394,.T.);
#11797=EDGE_CURVE('',#8939,#8937,#1395,.T.);
#11798=EDGE_CURVE('',#8941,#8942,#5703,.T.);
#11799=EDGE_CURVE('',#8942,#8940,#1396,.T.);
#11800=EDGE_CURVE('',#8941,#8939,#1397,.T.);
#11801=EDGE_CURVE('',#8943,#8944,#5704,.T.);
#11802=EDGE_CURVE('',#8944,#8942,#1398,.T.);
#11803=EDGE_CURVE('',#8943,#8941,#1399,.T.);
#11804=EDGE_CURVE('',#8945,#8946,#5705,.T.);
#11805=EDGE_CURVE('',#8947,#8945,#1400,.T.);
#11806=EDGE_CURVE('',#8948,#8947,#7562,.T.);
#11807=EDGE_CURVE('',#8948,#8946,#1401,.T.);
#11808=EDGE_CURVE('',#8946,#8944,#1402,.T.);
#11809=EDGE_CURVE('',#8945,#8943,#1403,.T.);
#11810=EDGE_CURVE('',#8931,#8912,#1404,.T.);
#11811=EDGE_CURVE('',#8927,#8948,#1405,.T.);
#11812=EDGE_CURVE('',#8923,#8925,#1406,.T.);
#11813=EDGE_CURVE('',#8911,#8932,#1407,.T.);
#11814=EDGE_CURVE('',#8926,#8924,#1408,.T.);
#11815=EDGE_CURVE('',#8947,#8928,#1409,.T.);
#11816=EDGE_CURVE('',#8949,#8950,#5706,.T.);
#11817=EDGE_CURVE('',#8950,#8951,#5707,.T.);
#11818=EDGE_CURVE('',#8951,#8952,#5708,.T.);
#11819=EDGE_CURVE('',#8952,#8953,#5709,.T.);
#11820=EDGE_CURVE('',#8953,#8954,#5710,.T.);
#11821=EDGE_CURVE('',#8954,#8949,#5711,.T.);
#11822=EDGE_CURVE('',#8955,#8956,#5712,.T.);
#11823=EDGE_CURVE('',#8956,#8949,#5713,.T.);
#11824=EDGE_CURVE('',#8955,#8954,#5714,.T.);
#11825=EDGE_CURVE('',#8957,#8955,#5715,.T.);
#11826=EDGE_CURVE('',#8957,#8953,#5716,.T.);
#11827=EDGE_CURVE('',#8958,#8957,#5717,.T.);
#11828=EDGE_CURVE('',#8958,#8952,#5718,.T.);
#11829=EDGE_CURVE('',#8959,#8958,#5719,.T.);
#11830=EDGE_CURVE('',#8959,#8951,#5720,.T.);
#11831=EDGE_CURVE('',#8960,#8959,#5721,.T.);
#11832=EDGE_CURVE('',#8960,#8950,#5722,.T.);
#11833=EDGE_CURVE('',#8956,#8960,#5723,.T.);
#16998=ORIENTED_EDGE('',*,*,#11756,.T.);
#16999=ORIENTED_EDGE('',*,*,#11757,.T.);
#17000=ORIENTED_EDGE('',*,*,#11758,.F.);
#17001=ORIENTED_EDGE('',*,*,#11759,.T.);
#17002=ORIENTED_EDGE('',*,*,#11760,.T.);
#17003=ORIENTED_EDGE('',*,*,#11761,.T.);
#17004=ORIENTED_EDGE('',*,*,#11756,.F.);
#17005=ORIENTED_EDGE('',*,*,#11762,.T.);
#17006=ORIENTED_EDGE('',*,*,#11763,.T.);
#17007=ORIENTED_EDGE('',*,*,#11764,.T.);
#17008=ORIENTED_EDGE('',*,*,#11760,.F.);
#17009=ORIENTED_EDGE('',*,*,#11765,.T.);
#17010=ORIENTED_EDGE('',*,*,#11766,.T.);
#17011=ORIENTED_EDGE('',*,*,#11767,.T.);
#17012=ORIENTED_EDGE('',*,*,#11763,.F.);
#17013=ORIENTED_EDGE('',*,*,#11768,.T.);
#17014=ORIENTED_EDGE('',*,*,#11769,.T.);
#17015=ORIENTED_EDGE('',*,*,#11770,.T.);
#17016=ORIENTED_EDGE('',*,*,#11766,.F.);
#17017=ORIENTED_EDGE('',*,*,#11771,.T.);
#17018=ORIENTED_EDGE('',*,*,#11772,.T.);
#17019=ORIENTED_EDGE('',*,*,#11773,.T.);
#17020=ORIENTED_EDGE('',*,*,#11769,.F.);
#17021=ORIENTED_EDGE('',*,*,#11774,.T.);
#17022=ORIENTED_EDGE('',*,*,#11775,.T.);
#17023=ORIENTED_EDGE('',*,*,#11776,.T.);
#17024=ORIENTED_EDGE('',*,*,#11772,.F.);
#17025=ORIENTED_EDGE('',*,*,#11777,.T.);
#17026=ORIENTED_EDGE('',*,*,#11778,.F.);
#17027=ORIENTED_EDGE('',*,*,#11779,.T.);
#17028=ORIENTED_EDGE('',*,*,#11780,.F.);
#17029=ORIENTED_EDGE('',*,*,#11781,.T.);
#17030=ORIENTED_EDGE('',*,*,#11782,.T.);
#17031=ORIENTED_EDGE('',*,*,#11783,.T.);
#17032=ORIENTED_EDGE('',*,*,#11784,.F.);
#17033=ORIENTED_EDGE('',*,*,#11785,.F.);
#17034=ORIENTED_EDGE('',*,*,#11786,.T.);
#17035=ORIENTED_EDGE('',*,*,#11787,.T.);
#17036=ORIENTED_EDGE('',*,*,#11782,.F.);
#17037=ORIENTED_EDGE('',*,*,#11788,.F.);
#17038=ORIENTED_EDGE('',*,*,#11789,.T.);
#17039=ORIENTED_EDGE('',*,*,#11790,.T.);
#17040=ORIENTED_EDGE('',*,*,#11786,.F.);
#17041=ORIENTED_EDGE('',*,*,#11791,.F.);
#17042=ORIENTED_EDGE('',*,*,#11792,.T.);
#17043=ORIENTED_EDGE('',*,*,#11793,.T.);
#17044=ORIENTED_EDGE('',*,*,#11789,.F.);
#17045=ORIENTED_EDGE('',*,*,#11794,.F.);
#17046=ORIENTED_EDGE('',*,*,#11795,.T.);
#17047=ORIENTED_EDGE('',*,*,#11796,.T.);
#17048=ORIENTED_EDGE('',*,*,#11792,.F.);
#17049=ORIENTED_EDGE('',*,*,#11797,.F.);
#17050=ORIENTED_EDGE('',*,*,#11798,.T.);
#17051=ORIENTED_EDGE('',*,*,#11799,.T.);
#17052=ORIENTED_EDGE('',*,*,#11795,.F.);
#17053=ORIENTED_EDGE('',*,*,#11800,.F.);
#17054=ORIENTED_EDGE('',*,*,#11801,.T.);
#17055=ORIENTED_EDGE('',*,*,#11802,.T.);
#17056=ORIENTED_EDGE('',*,*,#11798,.F.);
#17057=ORIENTED_EDGE('',*,*,#11803,.F.);
#17058=ORIENTED_EDGE('',*,*,#11804,.F.);
#17059=ORIENTED_EDGE('',*,*,#11805,.F.);
#17060=ORIENTED_EDGE('',*,*,#11806,.F.);
#17061=ORIENTED_EDGE('',*,*,#11807,.T.);
#17062=ORIENTED_EDGE('',*,*,#11804,.T.);
#17063=ORIENTED_EDGE('',*,*,#11808,.T.);
#17064=ORIENTED_EDGE('',*,*,#11801,.F.);
#17065=ORIENTED_EDGE('',*,*,#11809,.F.);
#17066=ORIENTED_EDGE('',*,*,#11810,.F.);
#17067=ORIENTED_EDGE('',*,*,#11783,.F.);
#17068=ORIENTED_EDGE('',*,*,#11787,.F.);
#17069=ORIENTED_EDGE('',*,*,#11790,.F.);
#17070=ORIENTED_EDGE('',*,*,#11793,.F.);
#17071=ORIENTED_EDGE('',*,*,#11796,.F.);
#17072=ORIENTED_EDGE('',*,*,#11799,.F.);
#17073=ORIENTED_EDGE('',*,*,#11802,.F.);
#17074=ORIENTED_EDGE('',*,*,#11808,.F.);
#17075=ORIENTED_EDGE('',*,*,#11807,.F.);
#17076=ORIENTED_EDGE('',*,*,#11811,.F.);
#17077=ORIENTED_EDGE('',*,*,#11779,.F.);
#17078=ORIENTED_EDGE('',*,*,#11812,.F.);
#17079=ORIENTED_EDGE('',*,*,#11777,.F.);
#17080=ORIENTED_EDGE('',*,*,#11774,.F.);
#17081=ORIENTED_EDGE('',*,*,#11771,.F.);
#17082=ORIENTED_EDGE('',*,*,#11768,.F.);
#17083=ORIENTED_EDGE('',*,*,#11765,.F.);
#17084=ORIENTED_EDGE('',*,*,#11762,.F.);
#17085=ORIENTED_EDGE('',*,*,#11759,.F.);
#17086=ORIENTED_EDGE('',*,*,#11813,.F.);
#17087=ORIENTED_EDGE('',*,*,#11757,.F.);
#17088=ORIENTED_EDGE('',*,*,#11761,.F.);
#17089=ORIENTED_EDGE('',*,*,#11764,.F.);
#17090=ORIENTED_EDGE('',*,*,#11767,.F.);
#17091=ORIENTED_EDGE('',*,*,#11770,.F.);
#17092=ORIENTED_EDGE('',*,*,#11773,.F.);
#17093=ORIENTED_EDGE('',*,*,#11776,.F.);
#17094=ORIENTED_EDGE('',*,*,#11814,.F.);
#17095=ORIENTED_EDGE('',*,*,#11781,.F.);
#17096=ORIENTED_EDGE('',*,*,#11815,.F.);
#17097=ORIENTED_EDGE('',*,*,#11805,.T.);
#17098=ORIENTED_EDGE('',*,*,#11809,.T.);
#17099=ORIENTED_EDGE('',*,*,#11803,.T.);
#17100=ORIENTED_EDGE('',*,*,#11800,.T.);
#17101=ORIENTED_EDGE('',*,*,#11797,.T.);
#17102=ORIENTED_EDGE('',*,*,#11794,.T.);
#17103=ORIENTED_EDGE('',*,*,#11791,.T.);
#17104=ORIENTED_EDGE('',*,*,#11788,.T.);
#17105=ORIENTED_EDGE('',*,*,#11785,.T.);
#17106=ORIENTED_EDGE('',*,*,#11816,.T.);
#17107=ORIENTED_EDGE('',*,*,#11817,.T.);
#17108=ORIENTED_EDGE('',*,*,#11818,.T.);
#17109=ORIENTED_EDGE('',*,*,#11819,.T.);
#17110=ORIENTED_EDGE('',*,*,#11820,.T.);
#17111=ORIENTED_EDGE('',*,*,#11821,.T.);
#17112=ORIENTED_EDGE('',*,*,#11811,.T.);
#17113=ORIENTED_EDGE('',*,*,#11806,.T.);
#17114=ORIENTED_EDGE('',*,*,#11815,.T.);
#17115=ORIENTED_EDGE('',*,*,#11780,.T.);
#17116=ORIENTED_EDGE('',*,*,#11778,.T.);
#17117=ORIENTED_EDGE('',*,*,#11814,.T.);
#17118=ORIENTED_EDGE('',*,*,#11775,.F.);
#17119=ORIENTED_EDGE('',*,*,#11812,.T.);
#17120=ORIENTED_EDGE('',*,*,#11822,.T.);
#17121=ORIENTED_EDGE('',*,*,#11823,.T.);
#17122=ORIENTED_EDGE('',*,*,#11821,.F.);
#17123=ORIENTED_EDGE('',*,*,#11824,.F.);
#17124=ORIENTED_EDGE('',*,*,#11825,.T.);
#17125=ORIENTED_EDGE('',*,*,#11824,.T.);
#17126=ORIENTED_EDGE('',*,*,#11820,.F.);
#17127=ORIENTED_EDGE('',*,*,#11826,.F.);
#17128=ORIENTED_EDGE('',*,*,#11827,.T.);
#17129=ORIENTED_EDGE('',*,*,#11826,.T.);
#17130=ORIENTED_EDGE('',*,*,#11819,.F.);
#17131=ORIENTED_EDGE('',*,*,#11828,.F.);
#17132=ORIENTED_EDGE('',*,*,#11829,.T.);
#17133=ORIENTED_EDGE('',*,*,#11828,.T.);
#17134=ORIENTED_EDGE('',*,*,#11818,.F.);
#17135=ORIENTED_EDGE('',*,*,#11830,.F.);
#17136=ORIENTED_EDGE('',*,*,#11831,.T.);
#17137=ORIENTED_EDGE('',*,*,#11830,.T.);
#17138=ORIENTED_EDGE('',*,*,#11817,.F.);
#17139=ORIENTED_EDGE('',*,*,#11832,.F.);
#17140=ORIENTED_EDGE('',*,*,#11833,.T.);
#17141=ORIENTED_EDGE('',*,*,#11832,.T.);
#17142=ORIENTED_EDGE('',*,*,#11816,.F.);
#17143=ORIENTED_EDGE('',*,*,#11823,.F.);
#17144=ORIENTED_EDGE('',*,*,#11833,.F.);
#17145=ORIENTED_EDGE('',*,*,#11822,.F.);
#17146=ORIENTED_EDGE('',*,*,#11825,.F.);
#17147=ORIENTED_EDGE('',*,*,#11827,.F.);
#17148=ORIENTED_EDGE('',*,*,#11829,.F.);
#17149=ORIENTED_EDGE('',*,*,#11831,.F.);
#17150=ORIENTED_EDGE('',*,*,#11810,.T.);
#17151=ORIENTED_EDGE('',*,*,#11758,.T.);
#17152=ORIENTED_EDGE('',*,*,#11813,.T.);
#17153=ORIENTED_EDGE('',*,*,#11784,.T.);
#20247=CYLINDRICAL_SURFACE('',#22951,4.51775);
#20248=CYLINDRICAL_SURFACE('',#22953,4.51775);
#20249=CYLINDRICAL_SURFACE('',#22954,4.51775);
#20250=CYLINDRICAL_SURFACE('',#22955,4.51775);
#20251=CYLINDRICAL_SURFACE('',#22956,4.51775);
#20252=CYLINDRICAL_SURFACE('',#22957,4.51775);
#20253=CYLINDRICAL_SURFACE('',#22958,4.51775);
#20254=CYLINDRICAL_SURFACE('',#22959,4.51775);
#20255=CYLINDRICAL_SURFACE('',#22961,5.0736);
#20256=CYLINDRICAL_SURFACE('',#22963,5.0736);
#20257=CYLINDRICAL_SURFACE('',#22964,5.0736);
#20258=CYLINDRICAL_SURFACE('',#22965,5.0736);
#20259=CYLINDRICAL_SURFACE('',#22966,5.0736);
#20260=CYLINDRICAL_SURFACE('',#22967,5.0736);
#20261=CYLINDRICAL_SURFACE('',#22968,5.0736);
#20262=CYLINDRICAL_SURFACE('',#22969,5.0736);
#20263=CYLINDRICAL_SURFACE('',#22971,5.0736);
#20264=CYLINDRICAL_SURFACE('',#22973,4.51775);
#21341=ADVANCED_FACE('',(#3221),#20247,.F.);
#21342=ADVANCED_FACE('',(#3222),#20248,.F.);
#21343=ADVANCED_FACE('',(#3223),#20249,.F.);
#21344=ADVANCED_FACE('',(#3224),#20250,.F.);
#21345=ADVANCED_FACE('',(#3225),#20251,.F.);
#21346=ADVANCED_FACE('',(#3226),#20252,.F.);
#21347=ADVANCED_FACE('',(#3227),#20253,.F.);
#21348=ADVANCED_FACE('',(#3228),#20254,.F.);
#21349=ADVANCED_FACE('',(#3229),#20255,.F.);
#21350=ADVANCED_FACE('',(#3230),#20256,.F.);
#21351=ADVANCED_FACE('',(#3231),#20257,.F.);
#21352=ADVANCED_FACE('',(#3232),#20258,.F.);
#21353=ADVANCED_FACE('',(#3233),#20259,.F.);
#21354=ADVANCED_FACE('',(#3234),#20260,.F.);
#21355=ADVANCED_FACE('',(#3235),#20261,.F.);
#21356=ADVANCED_FACE('',(#3236),#20262,.F.);
#21357=ADVANCED_FACE('',(#3237),#20263,.F.);
#21358=ADVANCED_FACE('',(#3238),#358,.F.);
#21359=ADVANCED_FACE('',(#3239),#359,.F.);
#21360=ADVANCED_FACE('',(#3240,#2355),#2497,.T.);
#21361=ADVANCED_FACE('',(#3241),#20264,.F.);
#21362=ADVANCED_FACE('',(#3242),#2498,.T.);
#21363=ADVANCED_FACE('',(#3243),#2499,.T.);
#21364=ADVANCED_FACE('',(#3244),#2500,.T.);
#21365=ADVANCED_FACE('',(#3245),#2501,.T.);
#21366=ADVANCED_FACE('',(#3246),#2502,.T.);
#21367=ADVANCED_FACE('',(#3247),#2503,.T.);
#21368=ADVANCED_FACE('',(#3248,#2356),#2504,.F.);
#21823=CLOSED_SHELL('',(#21341,#21342,#21343,#21344,#21345,#21346,#21347,
#21348,#21349,#21350,#21351,#21352,#21353,#21354,#21355,#21356,#21357,#21358,
#21359,#21360,#21361,#21362,#21363,#21364,#21365,#21366,#21367,#21368));
#22950=AXIS2_PLACEMENT_3D('',#68891,#26076,#26077);
#22951=AXIS2_PLACEMENT_3D('',#68892,#26078,#26079);
#22952=AXIS2_PLACEMENT_3D('',#68905,#26081,#26082);
#22953=AXIS2_PLACEMENT_3D('',#68916,#26083,#26084);
#22954=AXIS2_PLACEMENT_3D('',#68967,#26086,#26087);
#22955=AXIS2_PLACEMENT_3D('',#69018,#26089,#26090);
#22956=AXIS2_PLACEMENT_3D('',#69066,#26092,#26093);
#22957=AXIS2_PLACEMENT_3D('',#69117,#26095,#26096);
#22958=AXIS2_PLACEMENT_3D('',#69168,#26098,#26099);
#22959=AXIS2_PLACEMENT_3D('',#69216,#26101,#26102);
#22960=AXIS2_PLACEMENT_3D('',#69238,#26104,#26105);
#22961=AXIS2_PLACEMENT_3D('',#69258,#26106,#26107);
#22962=AXIS2_PLACEMENT_3D('',#69273,#26109,#26110);
#22963=AXIS2_PLACEMENT_3D('',#69283,#26111,#26112);
#22964=AXIS2_PLACEMENT_3D('',#69307,#26114,#26115);
#22965=AXIS2_PLACEMENT_3D('',#69332,#26117,#26118);
#22966=AXIS2_PLACEMENT_3D('',#69357,#26120,#26121);
#22967=AXIS2_PLACEMENT_3D('',#69381,#26123,#26124);
#22968=AXIS2_PLACEMENT_3D('',#69406,#26126,#26127);
#22969=AXIS2_PLACEMENT_3D('',#69431,#26129,#26130);
#22970=AXIS2_PLACEMENT_3D('',#69443,#26132,#26133);
#22971=AXIS2_PLACEMENT_3D('',#69449,#26134,#26135);
#22972=AXIS2_PLACEMENT_3D('',#70403,#26136,#26137);
#22973=AXIS2_PLACEMENT_3D('',#70416,#26144,#26145);
#22974=AXIS2_PLACEMENT_3D('',#70417,#26146,#26147);
#22975=AXIS2_PLACEMENT_3D('',#70423,#26151,#26152);
#22976=AXIS2_PLACEMENT_3D('',#70427,#26155,#26156);
#22977=AXIS2_PLACEMENT_3D('',#70431,#26159,#26160);
#22978=AXIS2_PLACEMENT_3D('',#70435,#26163,#26164);
#22979=AXIS2_PLACEMENT_3D('',#70439,#26167,#26168);
#22980=AXIS2_PLACEMENT_3D('',#70441,#26170,#26171);
#26076=DIRECTION('axis',(0.,0.,1.));
#26077=DIRECTION('refdir',(1.,0.,0.));
#26078=DIRECTION('center_axis',(0.,0.,-1.));
#26079=DIRECTION('ref_axis',(-0.346147419294793,0.938180134150982,0.));
#26080=DIRECTION('',(0.,0.,-1.));
#26081=DIRECTION('center_axis',(0.,0.,-1.));
#26082=DIRECTION('ref_axis',(1.,0.,0.));
#26083=DIRECTION('center_axis',(0.,0.,-1.));
#26084=DIRECTION('ref_axis',(1.,0.,0.));
#26085=DIRECTION('',(0.,0.,-1.));
#26086=DIRECTION('center_axis',(0.,0.,-1.));
#26087=DIRECTION('ref_axis',(1.,0.,0.));
#26088=DIRECTION('',(0.,0.,-1.));
#26089=DIRECTION('center_axis',(0.,0.,-1.));
#26090=DIRECTION('ref_axis',(1.,0.,0.));
#26091=DIRECTION('',(0.,0.,-1.));
#26092=DIRECTION('center_axis',(0.,0.,-1.));
#26093=DIRECTION('ref_axis',(1.,0.,0.));
#26094=DIRECTION('',(0.,0.,-1.));
#26095=DIRECTION('center_axis',(0.,0.,-1.));
#26096=DIRECTION('ref_axis',(1.,0.,0.));
#26097=DIRECTION('',(0.,0.,-1.));
#26098=DIRECTION('center_axis',(0.,0.,-1.));
#26099=DIRECTION('ref_axis',(1.,0.,0.));
#26100=DIRECTION('',(0.,0.,-1.));
#26101=DIRECTION('center_axis',(0.,0.,-1.));
#26102=DIRECTION('ref_axis',(0.938064160696058,-0.346461585774816,0.));
#26103=DIRECTION('',(0.,0.,-1.));
#26104=DIRECTION('center_axis',(0.,0.,-1.));
#26105=DIRECTION('ref_axis',(1.,0.,0.));
#26106=DIRECTION('center_axis',(0.,0.,-1.));
#26107=DIRECTION('ref_axis',(0.793491609261867,0.608581190993456,0.));
#26108=DIRECTION('',(1.22464679914735E-16,-2.66964461005383E-30,-1.));
#26109=DIRECTION('center_axis',(0.,0.,1.));
#26110=DIRECTION('ref_axis',(1.,-2.16768378774637E-14,0.));
#26111=DIRECTION('center_axis',(0.,0.,-1.));
#26112=DIRECTION('ref_axis',(1.,-2.16768378774637E-14,0.));
#26113=DIRECTION('',(1.22464679914735E-16,-2.66964461005383E-30,-1.));
#26114=DIRECTION('center_axis',(0.,0.,-1.));
#26115=DIRECTION('ref_axis',(1.,-2.16768378774637E-14,0.));
#26116=DIRECTION('',(1.22464679914735E-16,-2.66964461005383E-30,-1.));
#26117=DIRECTION('center_axis',(0.,0.,-1.));
#26118=DIRECTION('ref_axis',(1.,-2.16768378774637E-14,0.));
#26119=DIRECTION('',(1.22464679914735E-16,-2.66964461005383E-30,-1.));
#26120=DIRECTION('center_axis',(0.,0.,-1.));
#26121=DIRECTION('ref_axis',(1.,-2.16768378774637E-14,0.));
#26122=DIRECTION('',(1.22464679914735E-16,-2.66964461005383E-30,-1.));
#26123=DIRECTION('center_axis',(0.,0.,-1.));
#26124=DIRECTION('ref_axis',(1.,-2.16768378774637E-14,0.));
#26125=DIRECTION('',(1.22464679914735E-16,-2.66964461005383E-30,-1.));
#26126=DIRECTION('center_axis',(0.,0.,-1.));
#26127=DIRECTION('ref_axis',(1.,-2.16768378774637E-14,0.));
#26128=DIRECTION('',(1.22464679914735E-16,-2.66964461005383E-30,-1.));
#26129=DIRECTION('center_axis',(0.,0.,-1.));
#26130=DIRECTION('ref_axis',(-0.608751959302999,-0.793360606562211,0.));
#26131=DIRECTION('',(1.22464679914735E-16,-2.66964461005383E-30,-1.));
#26132=DIRECTION('center_axis',(0.,0.,-1.));
#26133=DIRECTION('ref_axis',(1.,-2.16768378774637E-14,0.));
#26134=DIRECTION('center_axis',(0.,0.,-1.));
#26135=DIRECTION('ref_axis',(1.,-2.16768378774637E-14,0.));
#26136=DIRECTION('center_axis',(0.,0.,1.));
#26137=DIRECTION('ref_axis',(1.,0.,0.));
#26138=DIRECTION('',(0.5,0.866025403784439,0.));
#26139=DIRECTION('',(-0.5,0.866025403784439,0.));
#26140=DIRECTION('',(-1.,0.,0.));
#26141=DIRECTION('',(-0.5,-0.866025403784439,0.));
#26142=DIRECTION('',(0.5,-0.866025403784439,0.));
#26143=DIRECTION('',(1.,-3.39346356420629E-16,0.));
#26144=DIRECTION('center_axis',(0.,0.,-1.));
#26145=DIRECTION('ref_axis',(1.,0.,0.));
#26146=DIRECTION('center_axis',(-3.39346356420629E-16,-1.,0.));
#26147=DIRECTION('ref_axis',(1.,-3.39346356420629E-16,0.));
#26148=DIRECTION('',(1.,-3.39346356420629E-16,0.));
#26149=DIRECTION('',(0.,0.,1.));
#26150=DIRECTION('',(0.,0.,1.));
#26151=DIRECTION('center_axis',(-0.866025403784439,-0.5,0.));
#26152=DIRECTION('ref_axis',(0.5,-0.866025403784439,0.));
#26153=DIRECTION('',(0.5,-0.866025403784439,0.));
#26154=DIRECTION('',(0.,0.,1.));
#26155=DIRECTION('center_axis',(-0.866025403784439,0.5,0.));
#26156=DIRECTION('ref_axis',(-0.5,-0.866025403784438,0.));
#26157=DIRECTION('',(-0.5,-0.866025403784439,0.));
#26158=DIRECTION('',(0.,0.,1.));
#26159=DIRECTION('center_axis',(0.,1.,0.));
#26160=DIRECTION('ref_axis',(-1.,0.,0.));
#26161=DIRECTION('',(-1.,0.,0.));
#26162=DIRECTION('',(0.,0.,1.));
#26163=DIRECTION('center_axis',(0.866025403784439,0.5,0.));
#26164=DIRECTION('ref_axis',(-0.5,0.866025403784439,0.));
#26165=DIRECTION('',(-0.5,0.866025403784439,0.));
#26166=DIRECTION('',(0.,0.,1.));
#26167=DIRECTION('center_axis',(0.866025403784439,-0.5,0.));
#26168=DIRECTION('ref_axis',(0.5,0.866025403784439,0.));
#26169=DIRECTION('',(0.5,0.866025403784439,0.));
#26170=DIRECTION('center_axis',(0.,0.,1.));
#26171=DIRECTION('ref_axis',(1.,0.,0.));
#68891=CARTESIAN_POINT('',(0.,0.,0.));
#68892=CARTESIAN_POINT('Origin',(0.,0.,4.));
#68893=CARTESIAN_POINT('',(-4.51054691465169,-0.000515110389415763,0.38741669750802));
#68894=CARTESIAN_POINT('',(-4.51874859034235,-0.000597354552748235,0.112583302491978));
#68895=CARTESIAN_POINT('',(-4.51775,5.53264807684796E-16,4.));
#68896=CARTESIAN_POINT('',(-3.43378788736191,2.93584158412995,0.));
#68897=CARTESIAN_POINT('Ctrl Pts',(-4.51874859034235,-0.000597354552748235,
0.112583302491978));
#68898=CARTESIAN_POINT('Ctrl Pts',(-4.51722457181931,0.322607764342177,
0.101221950551661));
#68899=CARTESIAN_POINT('Ctrl Pts',(-4.48139903614817,0.645891255334514,
0.0898605986113441));
#68900=CARTESIAN_POINT('Ctrl Pts',(-4.41220310426637,0.961201691623003,
0.0784992466710271));
#68901=CARTESIAN_POINT('Ctrl Pts',(-4.25283743035848,1.68739554150353,0.0523328311140182));
#68902=CARTESIAN_POINT('Ctrl Pts',(-3.91646501574702,2.37129788193745,0.0261664155570086));
#68903=CARTESIAN_POINT('Ctrl Pts',(-3.43378788736191,2.93584158412995,-2.08166817117217E-16));
#68904=CARTESIAN_POINT('',(3.44055068766013,2.93810645203836,-8.32667268468867E-16));
#68905=CARTESIAN_POINT('Origin',(0.,0.,0.));
#68906=CARTESIAN_POINT('Ctrl Pts',(3.44055068766013,2.93810645203836,-8.32667268468867E-16));
#68907=CARTESIAN_POINT('Ctrl Pts',(2.51857754810217,4.00873567447971,0.0500251109657056));
#68908=CARTESIAN_POINT('Ctrl Pts',(1.04980798302248,4.62287274287841,0.10005022193141));
#68909=CARTESIAN_POINT('Ctrl Pts',(-0.359976603224271,4.51112404046721,
0.150075332897117));
#68910=CARTESIAN_POINT('Ctrl Pts',(-1.83479629347494,4.39422023240758,0.202408164011137));
#68911=CARTESIAN_POINT('Ctrl Pts',(-3.24506337966313,3.48291388857057,0.254740995125157));
#68912=CARTESIAN_POINT('Ctrl Pts',(-3.96016577839605,2.18804786800098,0.307073826239177));
#68913=CARTESIAN_POINT('Ctrl Pts',(-4.32611438556047,1.52540931786942,0.333854783328791));
#68914=CARTESIAN_POINT('Ctrl Pts',(-4.5100126795522,0.762323836917479,0.360635740418406));
#68915=CARTESIAN_POINT('Ctrl Pts',(-4.51054691465169,-0.000515110389415763,
0.38741669750802));
#68916=CARTESIAN_POINT('Origin',(0.,0.,4.));
#68917=CARTESIAN_POINT('',(-4.52244050167421,-0.00276900106626683,1.38741669750802));
#68918=CARTESIAN_POINT('',(-4.5233994151039,0.0021134167823725,1.11258330249198));
#68919=CARTESIAN_POINT('',(-4.51775,5.53264807684796E-16,4.));
#68920=CARTESIAN_POINT('Ctrl Pts',(-4.5233994151039,0.0021134167823725,
1.11258330249198));
#68921=CARTESIAN_POINT('Ctrl Pts',(-4.52416026905118,0.130280331830068,
1.10805201945945));
#68922=CARTESIAN_POINT('Ctrl Pts',(-4.51917716893618,0.258387747461467,
1.10352073642693));
#68923=CARTESIAN_POINT('Ctrl Pts',(-4.50825644670978,0.385987082702882,
1.0989894533944));
#68924=CARTESIAN_POINT('Ctrl Pts',(-4.38213051111597,1.85966118637707,1.04665662228038));
#68925=CARTESIAN_POINT('Ctrl Pts',(-3.46401651516602,3.2655651297045,0.994323791166365));
#68926=CARTESIAN_POINT('Ctrl Pts',(-2.16517718342927,3.97324079579977,0.941990960052346));
#68927=CARTESIAN_POINT('Ctrl Pts',(-0.866337851692522,4.68091646189503,
0.889658128938326));
#68928=CARTESIAN_POINT('Ctrl Pts',(0.813226815831038,4.69036385075812,0.837325297824306));
#68929=CARTESIAN_POINT('Ctrl Pts',(2.11977950774785,3.99758999513324,0.784992466710287));
#68930=CARTESIAN_POINT('Ctrl Pts',(3.42633219966466,3.30481613950837,0.732659635596268));
#68931=CARTESIAN_POINT('Ctrl Pts',(4.35987291597477,1.90982103939552,0.680326804482248));
#68932=CARTESIAN_POINT('Ctrl Pts',(4.50321991349222,0.437577595733461,0.627993973368229));
#68933=CARTESIAN_POINT('Ctrl Pts',(4.64656691100967,-1.0346658479286,0.57566114225421));
#68934=CARTESIAN_POINT('Ctrl Pts',(3.99972018973448,-2.58415763513987,0.523328311140192));
#68935=CARTESIAN_POINT('Ctrl Pts',(2.85003205531654,-3.51527160715898,0.470995480026173));
#68936=CARTESIAN_POINT('Ctrl Pts',(1.7003439208986,-4.4463855791781,0.418662648912154));
#68937=CARTESIAN_POINT('Ctrl Pts',(0.0478143733379097,-4.75912173600502,
0.366329817798135));
#68938=CARTESIAN_POINT('Ctrl Pts',(-1.36123648115533,-4.3152078830999,0.313996986684115));
#68939=CARTESIAN_POINT('Ctrl Pts',(-2.77028733564855,-3.87129403019478,
0.261664155570096));
#68940=CARTESIAN_POINT('Ctrl Pts',(-3.93585949707434,-2.67073016755762,
0.209331324456076));
#68941=CARTESIAN_POINT('Ctrl Pts',(-4.34790497327718,-1.24589506757571,
0.156998493342058));
#68942=CARTESIAN_POINT('Ctrl Pts',(-4.46447347068682,-0.842806340108052,
0.142193429725364));
#68943=CARTESIAN_POINT('Ctrl Pts',(-4.52073455040284,-0.421768388741025,
0.127388366108671));
#68944=CARTESIAN_POINT('Ctrl Pts',(-4.51874859034235,-0.000597354552748235,
0.112583302491978));
#68945=CARTESIAN_POINT('Ctrl Pts',(-4.51054691465169,-0.000515110389415763,
0.38741669750802));
#68946=CARTESIAN_POINT('Ctrl Pts',(-4.51105663160901,-0.728344389129203,
0.412968571532425));
#68947=CARTESIAN_POINT('Ctrl Pts',(-4.3446466691941,-1.4559492437521,0.438520445556829));
#68948=CARTESIAN_POINT('Ctrl Pts',(-4.01017598625922,-2.09587333886935,
0.464072319581234));
#68949=CARTESIAN_POINT('Ctrl Pts',(-3.32514608411178,-3.40650282786799,
0.516405150695253));
#68950=CARTESIAN_POINT('Ctrl Pts',(-1.9351485685392,-4.34933610856308,0.568737981809272));
#68951=CARTESIAN_POINT('Ctrl Pts',(-0.463832664911,-4.50105515886306,0.621070812923292));
#68952=CARTESIAN_POINT('Ctrl Pts',(1.00748323871719,-4.65277420916302,0.673403644037311));
#68953=CARTESIAN_POINT('Ctrl Pts',(2.560117530401,-4.01337902906788,0.725736475151331));
#68954=CARTESIAN_POINT('Ctrl Pts',(3.49818631344856,-2.86985357730659,0.77806930626535));
#68955=CARTESIAN_POINT('Ctrl Pts',(4.43625509649613,-1.7263281255453,0.830402137379369));
#68956=CARTESIAN_POINT('Ctrl Pts',(4.75975837090746,-0.0786724021178761,
0.882734968493387));
#68957=CARTESIAN_POINT('Ctrl Pts',(4.32353285348464,1.33455667095541,0.935067799607406));
#68958=CARTESIAN_POINT('Ctrl Pts',(3.88730733606183,2.7477857440287,0.987400630721425));
#68959=CARTESIAN_POINT('Ctrl Pts',(2.69135302680487,3.92658816674785,1.03973346183545));
#68960=CARTESIAN_POINT('Ctrl Pts',(1.27193499135498,4.34236723513978,1.09206629294946));
#68961=CARTESIAN_POINT('Ctrl Pts',(-0.147483044094926,4.7581463035317,1.14439912406348));
#68962=CARTESIAN_POINT('Ctrl Pts',(-1.79036480573777,4.41090201759639,1.1967319551775));
#68963=CARTESIAN_POINT('Ctrl Pts',(-2.92016350112278,3.45636436650575,1.24906478629152));
#68964=CARTESIAN_POINT('Ctrl Pts',(-3.91577693325848,2.61519636835964,1.29518209003036));
#68965=CARTESIAN_POINT('Ctrl Pts',(-4.51294659780824,1.30242392182032,1.34129939376919));
#68966=CARTESIAN_POINT('Ctrl Pts',(-4.52244050167421,-0.00276900106626683,
1.38741669750802));
#68967=CARTESIAN_POINT('Origin',(0.,0.,4.));
#68968=CARTESIAN_POINT('',(-4.51698911071085,0.00388851918503852,2.38741669750802));
#68969=CARTESIAN_POINT('',(-4.51093362149631,0.00101330851266679,2.11258330249198));
#68970=CARTESIAN_POINT('',(-4.51775,5.53264807684796E-16,4.));
#68971=CARTESIAN_POINT('Ctrl Pts',(-4.51093362149631,0.00101330851266679,
2.11258330249198));
#68972=CARTESIAN_POINT('Ctrl Pts',(-4.51232811703185,0.680923530020972,
2.08871567281024));
#68973=CARTESIAN_POINT('Ctrl Pts',(-4.36790019846314,1.36027124256301,2.06484804312849));
#68974=CARTESIAN_POINT('Ctrl Pts',(-4.07455659430891,1.96770381197164,2.04098041344675));
#68975=CARTESIAN_POINT('Ctrl Pts',(-3.43136321904367,3.29957742036487,1.98864758233273));
#68976=CARTESIAN_POINT('Ctrl Pts',(-2.07224023608874,4.28571055146719,1.93631475121871));
#68977=CARTESIAN_POINT('Ctrl Pts',(-0.606537899693793,4.48397159897241,
1.88398192010469));
#68978=CARTESIAN_POINT('Ctrl Pts',(0.859164436701136,4.68223264647763,1.83164908899067));
#68979=CARTESIAN_POINT('Ctrl Pts',(2.43144612653608,4.09262161038578,1.77931625787665));
#68980=CARTESIAN_POINT('Ctrl Pts',(3.40536636602181,2.97949323501332,1.72698342676264));
#68981=CARTESIAN_POINT('Ctrl Pts',(4.37928660550757,1.86636485964083,1.67465059564862));
#68982=CARTESIAN_POINT('Ctrl Pts',(4.75484539464409,0.229719144987712,1.6223177645346));
#68983=CARTESIAN_POINT('Ctrl Pts',(4.36368967023442,-1.19666928711504,1.56998493342058));
#68984=CARTESIAN_POINT('Ctrl Pts',(3.97253394582476,-2.62305771921779,1.51765210230656));
#68985=CARTESIAN_POINT('Ctrl Pts',(2.81466370786892,-3.83918886877017,1.46531927119254));
#68986=CARTESIAN_POINT('Ctrl Pts',(1.40915332177568,-4.29979703199479,1.41298644007852));
#68987=CARTESIAN_POINT('Ctrl Pts',(0.00364293568242802,-4.76040519521942,
1.3606536089645));
#68988=CARTESIAN_POINT('Ctrl Pts',(-1.64950759854823,-4.46549037211628,
1.30832077785048));
#68989=CARTESIAN_POINT('Ctrl Pts',(-2.80901392804473,-3.54731082855424,
1.25598794673646));
#68990=CARTESIAN_POINT('Ctrl Pts',(-3.86812340827646,-2.70863264767388,
1.20818639865497));
#68991=CARTESIAN_POINT('Ctrl Pts',(-4.51537299162016,-1.34994888171753,
1.16038485057347));
#68992=CARTESIAN_POINT('Ctrl Pts',(-4.5233994151039,0.0021134167823725,
1.11258330249198));
#68993=CARTESIAN_POINT('Ctrl Pts',(-4.52244050167421,-0.00276900106626683,
1.38741669750802));
#68994=CARTESIAN_POINT('Ctrl Pts',(-4.52372005651789,-0.178678295071038,
1.39363222488321));
#68995=CARTESIAN_POINT('Ctrl Pts',(-4.51432465941186,-0.35444990932754,
1.39984775225839));
#68996=CARTESIAN_POINT('Ctrl Pts',(-4.49379103756964,-0.528910718243546,
1.40606327963358));
#68997=CARTESIAN_POINT('Ctrl Pts',(-4.32090424950433,-1.99781713565632,
1.4583961107476));
#68998=CARTESIAN_POINT('Ctrl Pts',(-3.3584150442465,-3.37379895423595,1.51072894186162));
#68999=CARTESIAN_POINT('Ctrl Pts',(-2.037860803389,-4.0399278796399,1.56306177297564));
#69000=CARTESIAN_POINT('Ctrl Pts',(-0.717306562531505,-4.70605680504386,
1.61539460408966));
#69001=CARTESIAN_POINT('Ctrl Pts',(0.961312713925656,-4.66233283727215,
1.66772743520368));
#69002=CARTESIAN_POINT('Ctrl Pts',(2.24539906972787,-3.92836571897045,1.72006026631769));
#69003=CARTESIAN_POINT('Ctrl Pts',(3.52948542553009,-3.19439860066874,1.77239309743171));
#69004=CARTESIAN_POINT('Ctrl Pts',(4.41903886067735,-1.77018833183704,1.82472592854573));
#69005=CARTESIAN_POINT('Ctrl Pts',(4.51522900816629,-0.294270957708535,
1.87705875965975));
#69006=CARTESIAN_POINT('Ctrl Pts',(4.61141915565522,1.18164641641996,1.92939159077377));
#69007=CARTESIAN_POINT('Ctrl Pts',(3.91424601548584,2.70927089584527,1.98172442188779));
#69008=CARTESIAN_POINT('Ctrl Pts',(2.73628580760446,3.60369609834798,2.03405725300181));
#69009=CARTESIAN_POINT('Ctrl Pts',(1.55832559972309,4.4981213008507,2.08639008411583));
#69010=CARTESIAN_POINT('Ctrl Pts',(-0.100421675870265,4.75934722643081,
2.13872291522985));
#69011=CARTESIAN_POINT('Ctrl Pts',(-1.49626358664302,4.2702551012346,2.19105574634387));
#69012=CARTESIAN_POINT('Ctrl Pts',(-2.89210549741577,3.78116297603839,2.24338857745789));
#69013=CARTESIAN_POINT('Ctrl Pts',(-4.02504204336792,2.54175280006585,2.29572140857191));
#69014=CARTESIAN_POINT('Ctrl Pts',(-4.38712504707582,1.10770899592287,2.34805423968593));
#69015=CARTESIAN_POINT('Ctrl Pts',(-4.47790602629514,0.748167400624681,
2.36117505895996));
#69016=CARTESIAN_POINT('Ctrl Pts',(-4.52023125554896,0.376391161643011,
2.37429587823399));
#69017=CARTESIAN_POINT('Ctrl Pts',(-4.51698911071085,0.00388851918503852,
2.38741669750802));
#69018=CARTESIAN_POINT('Origin',(0.,0.,4.));
#69019=CARTESIAN_POINT('',(-4.51234492774861,-0.00257476452032779,3.38741669750802));
#69020=CARTESIAN_POINT('',(-4.52027081060448,-0.00355576929457683,3.11258330249198));
#69021=CARTESIAN_POINT('',(-4.51775,5.53264807684796E-16,4.));
#69022=CARTESIAN_POINT('Ctrl Pts',(-4.52027081060448,-0.00355576929457683,
3.11258330249198));
#69023=CARTESIAN_POINT('Ctrl Pts',(-4.50971003274407,1.22072076070225,3.06937932616102));
#69024=CARTESIAN_POINT('Ctrl Pts',(-3.99354051828841,2.45284880293372,3.02617534983006));
#69025=CARTESIAN_POINT('Ctrl Pts',(-3.10547711214626,3.29088013555457,2.9829713734991));
#69026=CARTESIAN_POINT('Ctrl Pts',(-2.02976889732455,4.30598466811756,2.93063854238508));
#69027=CARTESIAN_POINT('Ctrl Pts',(-0.408403261408893,4.74285492731681,
2.87830571127106));
#69028=CARTESIAN_POINT('Ctrl Pts',(1.03168676818161,4.40562172719721,2.82597288015704));
#69029=CARTESIAN_POINT('Ctrl Pts',(2.4717767977721,4.06838852707761,2.77364004904302));
#69030=CARTESIAN_POINT('Ctrl Pts',(3.73059122103745,2.95705186763916,2.721307217929));
#69031=CARTESIAN_POINT('Ctrl Pts',(4.2437450475446,1.56987545160024,2.66897438681498));
#69032=CARTESIAN_POINT('Ctrl Pts',(4.75689887405174,0.182699035561331,2.61664155570096));
#69033=CARTESIAN_POINT('Ctrl Pts',(4.5243921038007,-1.48031713707804,2.56430872458694));
#69034=CARTESIAN_POINT('Ctrl Pts',(3.65046881853353,-2.67356621578173,2.51197589347292));
#69035=CARTESIAN_POINT('Ctrl Pts',(2.77654553326636,-3.86681529448543,2.4596430623589));
#69036=CARTESIAN_POINT('Ctrl Pts',(1.26120573298304,-4.59029727925343,2.40731023124489));
#69037=CARTESIAN_POINT('Ctrl Pts',(-0.216154740062777,-4.51964138893216,
2.35497740013087));
#69038=CARTESIAN_POINT('Ctrl Pts',(-1.69351521310859,-4.44898549861089,
2.30264456901685));
#69039=CARTESIAN_POINT('Ctrl Pts',(-3.1328963589169,-3.58419173320037,2.25031173790283));
#69040=CARTESIAN_POINT('Ctrl Pts',(-3.88895504803329,-2.31298780765304,
2.19797890678881));
#69041=CARTESIAN_POINT('Ctrl Pts',(-4.30019522790109,-1.62154660273587,
2.16951370535653));
#69042=CARTESIAN_POINT('Ctrl Pts',(-4.50927050719276,-0.809866601606811,
2.14104850392425));
#69043=CARTESIAN_POINT('Ctrl Pts',(-4.51093362149631,0.00101330851266679,
2.11258330249198));
#69044=CARTESIAN_POINT('Ctrl Pts',(-4.51698911071085,0.00388851918503852,
2.38741669750802));
#69045=CARTESIAN_POINT('Ctrl Pts',(-4.50729985128856,-1.10934821713655,
2.42662870934801));
#69046=CARTESIAN_POINT('Ctrl Pts',(-4.09063314279102,-2.22907270570801,
2.465840721188));
#69047=CARTESIAN_POINT('Ctrl Pts',(-3.34408434212355,-3.04811166820345,
2.50505273302798));
#69048=CARTESIAN_POINT('Ctrl Pts',(-2.34773117199973,-4.14121109587334,
2.557385564142));
#69049=CARTESIAN_POINT('Ctrl Pts',(-0.763795370288439,-4.69873251889968,
2.60971839525602));
#69050=CARTESIAN_POINT('Ctrl Pts',(0.697571505631126,-4.4707134324377,2.66205122637004));
#69051=CARTESIAN_POINT('Ctrl Pts',(2.15893838155069,-4.24269434597572,2.71438405748406));
#69052=CARTESIAN_POINT('Ctrl Pts',(3.49773633167853,-3.2291347500254,2.76671688859808));
#69053=CARTESIAN_POINT('Ctrl Pts',(4.11372028899329,-1.88446020659954,2.8190497197121));
#69054=CARTESIAN_POINT('Ctrl Pts',(4.72970424630805,-0.539785663173669,
2.87138255082612));
#69055=CARTESIAN_POINT('Ctrl Pts',(4.62287421080972,1.13600382772776,2.92371538194014));
#69056=CARTESIAN_POINT('Ctrl Pts',(3.84112705187867,2.39157432571858,2.97604821305416));
#69057=CARTESIAN_POINT('Ctrl Pts',(3.05937989294762,3.6471448237094,3.02838104416818));
#69058=CARTESIAN_POINT('Ctrl Pts',(1.60271561058387,4.48249632878962,3.08071387528219));
#69059=CARTESIAN_POINT('Ctrl Pts',(0.124224136080841,4.52310215772866,3.13304670639621));
#69060=CARTESIAN_POINT('Ctrl Pts',(-1.35426733842219,4.56370798666771,3.18537953751023));
#69061=CARTESIAN_POINT('Ctrl Pts',(-2.85458600506451,3.80956813946558,3.23771236862425));
#69062=CARTESIAN_POINT('Ctrl Pts',(-3.70406963378462,2.5987983669013,3.29004519973827));
#69063=CARTESIAN_POINT('Ctrl Pts',(-4.2309249653141,1.84787099365534,3.32250236566152));
#69064=CARTESIAN_POINT('Ctrl Pts',(-4.50743256748542,0.921298090727453,
3.35495953158477));
#69065=CARTESIAN_POINT('Ctrl Pts',(-4.51234492774861,-0.00257476452032779,
3.38741669750802));
#69066=CARTESIAN_POINT('Origin',(0.,0.,4.));
#69067=CARTESIAN_POINT('',(-4.52478583629221,-0.000271302356462328,4.38741669750802));
#69068=CARTESIAN_POINT('',(-4.51939464917808,0.00373292266216646,4.11258330249198));
#69069=CARTESIAN_POINT('',(-4.51775,5.53264807684796E-16,4.));
#69070=CARTESIAN_POINT('Ctrl Pts',(-4.51939464917808,0.00373292266216647,
4.11258330249198));
#69071=CARTESIAN_POINT('Ctrl Pts',(-4.52195179175284,0.293129143485266,
4.10237581062582));
#69072=CARTESIAN_POINT('Ctrl Pts',(-4.49647546580418,0.582077227182858,
4.09216831875966));
#69073=CARTESIAN_POINT('Ctrl Pts',(-4.44131034778915,0.865241438283023,
4.0819608268935));
#69074=CARTESIAN_POINT('Ctrl Pts',(-4.15848408230504,2.31699717136045,4.02962799577948));
#69075=CARTESIAN_POINT('Ctrl Pts',(-3.09528361658689,3.61672297535275,3.97729516466546));
#69076=CARTESIAN_POINT('Ctrl Pts',(-1.72839087618034,4.18169168234348,3.92496233355144));
#69077=CARTESIAN_POINT('Ctrl Pts',(-0.361498135773788,4.7466603893342,3.87262950243742));
#69078=CARTESIAN_POINT('Ctrl Pts',(1.30908687932117,4.57687199932334,3.8202966713234));
#69079=CARTESIAN_POINT('Ctrl Pts',(2.5343636726828,3.74845049626232,3.76796384020938));
#69080=CARTESIAN_POINT('Ctrl Pts',(3.75964046604444,2.9200289932013,3.71563100909536));
#69081=CARTESIAN_POINT('Ctrl Pts',(4.53960903767275,1.43297437709012,3.66329817798134));
#69082=CARTESIAN_POINT('Ctrl Pts',(4.52457341059044,-0.0459980138823182,
3.61096534686733));
#69083=CARTESIAN_POINT('Ctrl Pts',(4.50953778350813,-1.52497040485477,3.55863251575331));
#69084=CARTESIAN_POINT('Ctrl Pts',(3.69949795771518,-2.99586057068848,3.50629968463929));
#69085=CARTESIAN_POINT('Ctrl Pts',(2.45763224901275,-3.79920044943065,3.45396685352527));
#69086=CARTESIAN_POINT('Ctrl Pts',(1.21576654031032,-4.60254032817281,3.40163402241125));
#69087=CARTESIAN_POINT('Ctrl Pts',(-0.457925051301578,-4.73832991982345,
3.34930119129723));
#69088=CARTESIAN_POINT('Ctrl Pts',(-1.81304922569253,-4.1456884652134,3.29696836018321));
#69089=CARTESIAN_POINT('Ctrl Pts',(-3.16817340008348,-3.55304701060334,
3.24463552906919));
#69090=CARTESIAN_POINT('Ctrl Pts',(-4.20473015725347,-2.23197450973259,
3.19230269795517));
#69091=CARTESIAN_POINT('Ctrl Pts',(-4.45798313897459,-0.774768856333857,
3.13996986684115));
#69092=CARTESIAN_POINT('Ctrl Pts',(-4.50216018126897,-0.520576248830078,
3.1308410120581));
#69093=CARTESIAN_POINT('Ctrl Pts',(-4.52250226742098,-0.262241279420579,
3.12171215727504));
#69094=CARTESIAN_POINT('Ctrl Pts',(-4.52027081060448,-0.00355576929457683,
3.11258330249198));
#69095=CARTESIAN_POINT('Ctrl Pts',(-4.51234492774861,-0.00257476452032779,
3.38741669750802));
#69096=CARTESIAN_POINT('Ctrl Pts',(-4.51535309020244,-0.568323098591327,
3.40729236269879));
#69097=CARTESIAN_POINT('Ctrl Pts',(-4.41651517435603,-1.13305893603127,
3.42716802788956));
#69098=CARTESIAN_POINT('Ctrl Pts',(-4.21095206217547,-1.65582834772821,
3.44704369308033));
#69099=CARTESIAN_POINT('Ctrl Pts',(-3.66970227104832,-3.032285591867,3.49937652419435));
#69100=CARTESIAN_POINT('Ctrl Pts',(-2.3885540979961,-4.11780038221814,3.55170935530837));
#69101=CARTESIAN_POINT('Ctrl Pts',(-0.941905499312602,-4.42568625369714,
3.60404218642239));
#69102=CARTESIAN_POINT('Ctrl Pts',(0.504743099370899,-4.73357212517614,
3.65637501753641));
#69103=CARTESIAN_POINT('Ctrl Pts',(2.11689212368568,-4.263829077783,3.70870784865043));
#69104=CARTESIAN_POINT('Ctrl Pts',(3.17174063018436,-3.22706463608245,3.76104067976445));
#69105=CARTESIAN_POINT('Ctrl Pts',(4.22658913668306,-2.19030019438189,3.81337351087847));
#69106=CARTESIAN_POINT('Ctrl Pts',(4.72413712536563,-0.586514358373886,
3.86570634199248));
#69107=CARTESIAN_POINT('Ctrl Pts',(4.44131082922502,0.865241532073468,3.9180391731065));
#69108=CARTESIAN_POINT('Ctrl Pts',(4.15848453308441,2.31699742252081,3.97037200422052));
#69109=CARTESIAN_POINT('Ctrl Pts',(3.09528395212065,3.61672336740751,4.02270483533454));
#69110=CARTESIAN_POINT('Ctrl Pts',(1.7283910635404,4.18169213563993,4.07503766644856));
#69111=CARTESIAN_POINT('Ctrl Pts',(0.361498174960155,4.74666090387236,4.12737049756258));
#69112=CARTESIAN_POINT('Ctrl Pts',(-1.30908702123658,4.5768724954505,4.1797033286766));
#69113=CARTESIAN_POINT('Ctrl Pts',(-2.5343639474132,3.74845090259061,4.23203615979062));
#69114=CARTESIAN_POINT('Ctrl Pts',(-3.74701372251171,2.9285666488301,4.28382967236309));
#69115=CARTESIAN_POINT('Ctrl Pts',(-4.52348622608021,1.46355441369542,4.33562318493555));
#69116=CARTESIAN_POINT('Ctrl Pts',(-4.52478583629221,-0.000271302356462328,
4.38741669750802));
#69117=CARTESIAN_POINT('Origin',(0.,0.,4.));
#69118=CARTESIAN_POINT('',(-4.51292607061429,0.0029183530353194,5.38741669750802));
#69119=CARTESIAN_POINT('',(-4.51119223387812,-0.00146992377155156,5.11258330249198));
#69120=CARTESIAN_POINT('',(-4.51775,5.53264807684796E-16,4.));
#69121=CARTESIAN_POINT('Ctrl Pts',(-4.51119223387812,-0.00146992377155156,
5.11258330249198));
#69122=CARTESIAN_POINT('Ctrl Pts',(-4.50867979289825,0.840016500418339,
5.0830394639766));
#69123=CARTESIAN_POINT('Ctrl Pts',(-4.28245206788243,1.68275768437228,5.05349562546122));
#69124=CARTESIAN_POINT('Ctrl Pts',(-3.84112663548136,2.39157406650585,5.02395178694585));
#69125=CARTESIAN_POINT('Ctrl Pts',(-3.05937956127687,3.64714442841863,4.97161895583183));
#69126=CARTESIAN_POINT('Ctrl Pts',(-1.60271543685273,4.48249584288365,4.9192861247178));
#69127=CARTESIAN_POINT('Ctrl Pts',(-0.124224122626221,4.52310166740692,
4.86695329360379));
#69128=CARTESIAN_POINT('Ctrl Pts',(1.3542671916003,4.56370749193019,4.81462046248977));
#69129=CARTESIAN_POINT('Ctrl Pts',(2.85458569562921,3.80956772651169,4.76228763137575));
#69130=CARTESIAN_POINT('Ctrl Pts',(3.70406923227031,2.59879808520239,4.70995480026173));
#69131=CARTESIAN_POINT('Ctrl Pts',(4.5535527689114,1.3880284438931,4.65762196914771));
#69132=CARTESIAN_POINT('Ctrl Pts',(4.7522013381647,-0.279371073306991,4.60528913803369));
#69133=CARTESIAN_POINT('Ctrl Pts',(4.21095160570608,-1.65582816824236,4.55295630691967));
#69134=CARTESIAN_POINT('Ctrl Pts',(3.66970187324747,-3.03228526317774,4.50062347580565));
#69135=CARTESIAN_POINT('Ctrl Pts',(2.38855383907694,-4.11779993584839,4.44829064469163));
#69136=CARTESIAN_POINT('Ctrl Pts',(0.94190539721171,-4.42568577395046,4.39595781357761));
#69137=CARTESIAN_POINT('Ctrl Pts',(-0.50474304465354,-4.73357161205254,
4.34362498246359));
#69138=CARTESIAN_POINT('Ctrl Pts',(-2.11689189421349,-4.263828615586,4.29129215134958));
#69139=CARTESIAN_POINT('Ctrl Pts',(-3.17174028636843,-3.22706428627144,
4.23895932023556));
#69140=CARTESIAN_POINT('Ctrl Pts',(-4.02084104068784,-2.3925203076111,4.1968339809877));
#69141=CARTESIAN_POINT('Ctrl Pts',(-4.50884156719875,-1.19057750531243,
4.15470864173984));
#69142=CARTESIAN_POINT('Ctrl Pts',(-4.51939464917808,0.00373292266216647,
4.11258330249198));
#69143=CARTESIAN_POINT('Ctrl Pts',(-4.52478583629221,-0.000271302356462328,
4.38741669750802));
#69144=CARTESIAN_POINT('Ctrl Pts',(-4.52479936895005,-0.0155139130822968,
4.38795601604957));
#69145=CARTESIAN_POINT('Ctrl Pts',(-4.52472885144687,-0.030756395156677,
4.38849533459112));
#69146=CARTESIAN_POINT('Ctrl Pts',(-4.52457390104248,-0.0459980188636215,
4.38903465313267));
#69147=CARTESIAN_POINT('Ctrl Pts',(-4.50953827233865,-1.52497057016008,
4.44136748424669));
#69148=CARTESIAN_POINT('Ctrl Pts',(-3.69949835877446,-2.99586089545507,
4.49370031536071));
#69149=CARTESIAN_POINT('Ctrl Pts',(-2.45763251543912,-3.79920086127216,
4.54603314647473));
#69150=CARTESIAN_POINT('Ctrl Pts',(-1.21576667210378,-4.60254082708924,
4.59836597758875));
#69151=CARTESIAN_POINT('Ctrl Pts',(0.45792510100271,-4.73833043342844,4.65069880870277));
#69152=CARTESIAN_POINT('Ctrl Pts',(1.81304942226226,-4.14568891458885,4.70303163981679));
#69153=CARTESIAN_POINT('Ctrl Pts',(3.16817374352182,-3.55304739574926,4.75536447093081));
#69154=CARTESIAN_POINT('Ctrl Pts',(4.20473061293445,-2.23197475173087,4.80769730204483));
#69155=CARTESIAN_POINT('Ctrl Pts',(4.45798362215519,-0.774768940348221,
4.86003013315885));
#69156=CARTESIAN_POINT('Ctrl Pts',(4.71123663137592,0.682436871034428,4.91236296427287));
#69157=CARTESIAN_POINT('Ctrl Pts',(4.18118578040478,2.27577584978132,4.96469579538688));
#69158=CARTESIAN_POINT('Ctrl Pts',(3.10547744889356,3.29088049233953,5.0170286265009));
#69159=CARTESIAN_POINT('Ctrl Pts',(2.02976911738235,4.30598513489774,5.06936145761492));
#69160=CARTESIAN_POINT('Ctrl Pts',(0.408403305331062,4.74285544126724,5.12169428872895));
#69161=CARTESIAN_POINT('Ctrl Pts',(-1.03168688021991,4.40562220466712,5.17402711984297));
#69162=CARTESIAN_POINT('Ctrl Pts',(-2.47177706577088,4.068388968067,5.22635995095699));
#69163=CARTESIAN_POINT('Ctrl Pts',(-3.73059162482154,2.95705218849725,5.278692782071));
#69164=CARTESIAN_POINT('Ctrl Pts',(-4.2437455072054,1.56987562195304,5.33102561318502));
#69165=CARTESIAN_POINT('Ctrl Pts',(-4.42806131327582,1.07162631350615,5.34982264129268));
#69166=CARTESIAN_POINT('Ctrl Pts',(-4.51617798535533,0.537790377713164,
5.36861966940035));
#69167=CARTESIAN_POINT('Ctrl Pts',(-4.51292607061429,0.0029183530353194,
5.38741669750802));
#69168=CARTESIAN_POINT('Origin',(0.,0.,4.));
#69169=CARTESIAN_POINT('',(-4.51611343680291,-0.0038242599945422,6.38741669750802));
#69170=CARTESIAN_POINT('',(-4.52399690261043,-0.00167256832429505,6.11258330249198));
#69171=CARTESIAN_POINT('',(-4.51775,5.53264807684796E-16,4.));
#69172=CARTESIAN_POINT('Ctrl Pts',(-4.52399690261043,-0.00167256832429505,
6.11258330249198));
#69173=CARTESIAN_POINT('Ctrl Pts',(-4.5173342997898,1.3804594726294,6.06370311732738));
#69174=CARTESIAN_POINT('Ctrl Pts',(-3.83652995787924,2.76828008382611,6.01482293216279));
#69175=CARTESIAN_POINT('Ctrl Pts',(-2.73628551041168,3.60369570881218,5.96594274699819));
#69176=CARTESIAN_POINT('Ctrl Pts',(-1.55832542986843,4.49812081512447,5.91360991588417));
#69177=CARTESIAN_POINT('Ctrl Pts',(0.100421664862097,4.75934671033683,5.86127708477015));
#69178=CARTESIAN_POINT('Ctrl Pts',(1.49626342410919,4.27025463771519,5.80894425365613));
#69179=CARTESIAN_POINT('Ctrl Pts',(2.89210518335629,3.78116256509354,5.75661142254211));
#69180=CARTESIAN_POINT('Ctrl Pts',(4.02504160711995,2.54175252463788,5.7042785914281));
#69181=CARTESIAN_POINT('Ctrl Pts',(4.3871245717083,1.10770887619882,5.65194576031408));
#69182=CARTESIAN_POINT('Ctrl Pts',(4.74920753629665,-0.326334772240243,
5.59961292920006));
#69183=CARTESIAN_POINT('Ctrl Pts',(4.34043704170966,-1.95501202866272,5.54728009808604));
#69184=CARTESIAN_POINT('Ctrl Pts',(3.34408397951354,-3.04811133798521,5.49494726697202));
#69185=CARTESIAN_POINT('Ctrl Pts',(2.34773091731743,-4.14121064730769,5.442614435858));
#69186=CARTESIAN_POINT('Ctrl Pts',(0.763795287512193,-4.6987320095302,5.39028160474398));
#69187=CARTESIAN_POINT('Ctrl Pts',(-0.697571429950846,-4.47071294770401,
5.33794877362996));
#69188=CARTESIAN_POINT('Ctrl Pts',(-2.15893814741389,-4.24269388587781,
5.28561594251594));
#69189=CARTESIAN_POINT('Ctrl Pts',(-3.49773595253472,-3.22913440000291,
5.23328311140192));
#69190=CARTESIAN_POINT('Ctrl Pts',(-4.11371984310272,-1.88446000238519,
5.1809502802879));
#69191=CARTESIAN_POINT('Ctrl Pts',(-4.3819578119688,-1.29890454431857,5.15816128768926));
#69192=CARTESIAN_POINT('Ctrl Pts',(-4.51313023522704,-0.650560524599824,
5.13537229509062));
#69193=CARTESIAN_POINT('Ctrl Pts',(-4.51119223387812,-0.00146992377155156,
5.11258330249198));
#69194=CARTESIAN_POINT('Ctrl Pts',(-4.51292607061429,0.0029183530353194,
5.38741669750802));
#69195=CARTESIAN_POINT('Ctrl Pts',(-4.50712432517217,-0.95134754210846,
5.42095250051437));
#69196=CARTESIAN_POINT('Ctrl Pts',(-4.21049476107502,-1.90891132639337,
5.45448830352073));
#69197=CARTESIAN_POINT('Ctrl Pts',(-3.65046921487666,-2.67356650591896,
5.48802410652708));
#69198=CARTESIAN_POINT('Ctrl Pts',(-2.776545834447,-3.86681571372806,5.5403569376411));
#69199=CARTESIAN_POINT('Ctrl Pts',(-1.26120586787061,-4.5902977758276,5.59268976875511));
#69200=CARTESIAN_POINT('Ctrl Pts',(0.216154764597121,-4.51964187827841,
5.64502259986913));
#69201=CARTESIAN_POINT('Ctrl Pts',(1.69351539706486,-4.44898598072923,5.69735543098315));
#69202=CARTESIAN_POINT('Ctrl Pts',(3.13289669542393,-3.58419212353131,5.74968826209718));
#69203=CARTESIAN_POINT('Ctrl Pts',(3.88895546769304,-2.31298805942388,5.8020210932112));
#69204=CARTESIAN_POINT('Ctrl Pts',(4.64501423996215,-1.04178399531645,5.85435392432522));
#69205=CARTESIAN_POINT('Ctrl Pts',(4.71775048614129,0.635830275700497,5.90668675543923));
#69206=CARTESIAN_POINT('Ctrl Pts',(4.07455703922814,1.96770402713248,5.95901958655325));
#69207=CARTESIAN_POINT('Ctrl Pts',(3.43136359231499,3.29957777856446,6.01135241766727));
#69208=CARTESIAN_POINT('Ctrl Pts',(2.07224045230956,4.28571101041149,6.0636852487813));
#69209=CARTESIAN_POINT('Ctrl Pts',(0.606537960019231,4.4839720817303,6.11601807989532));
#69210=CARTESIAN_POINT('Ctrl Pts',(-0.859164532271093,4.68223315304911,
6.16835091100933));
#69211=CARTESIAN_POINT('Ctrl Pts',(-2.43144637684631,4.0926220638397,6.22068374212335));
#69212=CARTESIAN_POINT('Ctrl Pts',(-3.4053667262744,2.97949356381203,6.27301657323736));
#69213=CARTESIAN_POINT('Ctrl Pts',(-4.11503346658856,2.16838999191388,6.31114994799425));
#69214=CARTESIAN_POINT('Ctrl Pts',(-4.506994027605,1.07931947572563,6.34928332275114));
#69215=CARTESIAN_POINT('Ctrl Pts',(-4.51611343680291,-0.0038242599945422,
6.38741669750802));
#69216=CARTESIAN_POINT('Origin',(0.,0.,4.));
#69217=CARTESIAN_POINT('',(-4.52286359173795,0.00246468782935438,7.38741669750802));
#69218=CARTESIAN_POINT('',(-4.51483246697105,0.00361950456559231,7.11258330249198));
#69219=CARTESIAN_POINT('',(-4.51775,5.53264807684796E-16,4.));
#69220=CARTESIAN_POINT('',(3.43378788736184,2.93584158413003,8.));
#69221=CARTESIAN_POINT('Ctrl Pts',(-4.52286359173795,0.00246468782935438,
7.38741669750802));
#69222=CARTESIAN_POINT('Ctrl Pts',(-4.514736621556,-1.33289820095304,7.43461263832996));
#69223=CARTESIAN_POINT('Ctrl Pts',(-3.88687106704568,-2.67555385687553,
7.48180857915189));
#69224=CARTESIAN_POINT('Ctrl Pts',(-2.85003294005483,-3.51527175392636,
7.52900451997383));
#69225=CARTESIAN_POINT('Ctrl Pts',(-1.70034350389957,-4.44638604308903,
7.58133735108785));
#69226=CARTESIAN_POINT('Ctrl Pts',(-0.0478099810187527,-4.759123220785,
7.63367018220187));
#69227=CARTESIAN_POINT('Ctrl Pts',(1.3612375474742,-4.31520832020808,7.68600301331589));
#69228=CARTESIAN_POINT('Ctrl Pts',(2.77028507596716,-3.87129341963115,7.73833584442991));
#69229=CARTESIAN_POINT('Ctrl Pts',(3.93584661007225,-2.67072644078133,7.79066867554392));
#69230=CARTESIAN_POINT('Ctrl Pts',(4.34789968202776,-1.24589357093064,7.84300150665794));
#69231=CARTESIAN_POINT('Ctrl Pts',(4.55392621800552,-0.533477136005289,
7.86916792221495));
#69232=CARTESIAN_POINT('Ctrl Pts',(4.57157563844588,0.235005771670285,7.89533433777196));
#69233=CARTESIAN_POINT('Ctrl Pts',(4.41221033788124,0.961199526155991,7.92150075332897));
#69234=CARTESIAN_POINT('Ctrl Pts',(4.2528450373166,1.6873932806417,7.94766716888598));
#69235=CARTESIAN_POINT('Ctrl Pts',(3.91646501574697,2.37129788193754,7.97383358444299));
#69236=CARTESIAN_POINT('Ctrl Pts',(3.43378788736183,2.93584158413004,8.));
#69237=CARTESIAN_POINT('',(-3.44054916109511,2.9381068161154,8.));
#69238=CARTESIAN_POINT('Origin',(0.,0.,8.));
#69239=CARTESIAN_POINT('Ctrl Pts',(-3.44054916109511,2.9381068161154,8.));
#69240=CARTESIAN_POINT('Ctrl Pts',(-2.51857342159112,4.00873681403696,7.94997488903429));
#69241=CARTESIAN_POINT('Ctrl Pts',(-1.04980743191293,4.62287257548397,7.89994977806859));
#69242=CARTESIAN_POINT('Ctrl Pts',(0.359975956906261,4.51112341871505,7.84992466710289));
#69243=CARTESIAN_POINT('Ctrl Pts',(1.83479439449057,4.39421913533762,7.79759183598887));
#69244=CARTESIAN_POINT('Ctrl Pts',(3.24506283044465,3.48291324925361,7.74525900487485));
#69245=CARTESIAN_POINT('Ctrl Pts',(3.96016560277148,2.18804756351099,7.69292617376083));
#69246=CARTESIAN_POINT('Ctrl Pts',(4.67526837509831,0.893181877768381,7.64059334264681));
#69247=CARTESIAN_POINT('Ctrl Pts',(4.69520548379788,-0.785243607632836,
7.58826051153279));
#69248=CARTESIAN_POINT('Ctrl Pts',(4.01017546547555,-2.09587300826054,7.53592768041877));
#69249=CARTESIAN_POINT('Ctrl Pts',(3.32514544715321,-3.40650240888826,7.48359484930475));
#69250=CARTESIAN_POINT('Ctrl Pts',(1.93514830180898,-4.34933572474246,7.43126201819073));
#69251=CARTESIAN_POINT('Ctrl Pts',(0.463832634566904,-4.50105475907159,
7.37892918707671));
#69252=CARTESIAN_POINT('Ctrl Pts',(-1.00748303267517,-4.65277379340072,
7.32659635596269));
#69253=CARTESIAN_POINT('Ctrl Pts',(-2.56011722181508,-4.01337854620477,
7.27426352484867));
#69254=CARTESIAN_POINT('Ctrl Pts',(-3.49818593160913,-2.86985320272758,
7.22193069373465));
#69255=CARTESIAN_POINT('Ctrl Pts',(-4.15153848320893,-2.0734028007694,7.18548156332043));
#69256=CARTESIAN_POINT('Ctrl Pts',(-4.50676902168756,-1.0324019249735,7.14903243290621));
#69257=CARTESIAN_POINT('Ctrl Pts',(-4.51483246697105,0.00361950456559231,
7.11258330249198));
#69258=CARTESIAN_POINT('Origin',(0.,0.,10.2083368446371));
#69259=CARTESIAN_POINT('',(-5.0799445016814,0.00237344505285342,0.791663155362921));
#69260=CARTESIAN_POINT('',(-5.06551066928822,-0.000578487979983568,0.708336844637072));
#69261=CARTESIAN_POINT('',(-5.0736,1.10600941455115E-13,10.2083368446371));
#69262=CARTESIAN_POINT('',(1.31303618635654,-4.9007502418832,0.));
#69263=CARTESIAN_POINT('Ctrl Pts',(-5.06551066928822,-0.000578487979984235,
0.708336844637072));
#69264=CARTESIAN_POINT('Ctrl Pts',(-5.06491070355288,0.856117806205452,
0.681555887547458));
#69265=CARTESIAN_POINT('Ctrl Pts',(-4.45481520994778,3.38770743142078,0.602442099343825));
#69266=CARTESIAN_POINT('Ctrl Pts',(-0.476761969141785,5.95830217192949,
0.470995480026171));
#69267=CARTESIAN_POINT('Ctrl Pts',(4.70955374493753,3.67573393888292,0.313996986684114));
#69268=CARTESIAN_POINT('Ctrl Pts',(5.49957691269067,-0.955274817987675,
0.183164908899066));
#69269=CARTESIAN_POINT('Ctrl Pts',(3.61105296193539,-3.84612671226304,0.0784992466710263));
#69270=CARTESIAN_POINT('Ctrl Pts',(2.11876087752236,-4.68487601374969,0.0261664155570096));
#69271=CARTESIAN_POINT('Ctrl Pts',(1.31303618635654,-4.90075024188321,0.));
#69272=CARTESIAN_POINT('',(-1.31785621200034,-4.9071451662202,1.75207071073658E-15));
#69273=CARTESIAN_POINT('Origin',(0.,0.,0.));
#69274=CARTESIAN_POINT('Ctrl Pts',(-5.0799445016814,0.00237344505285278,
0.791663155362921));
#69275=CARTESIAN_POINT('Ctrl Pts',(-5.08079896874729,0.146309621287887,
0.787131872330397));
#69276=CARTESIAN_POINT('Ctrl Pts',(-5.01057089916491,1.95175929947146,0.730267758183854));
#69277=CARTESIAN_POINT('Ctrl Pts',(-2.85914249825567,5.24623219278067,0.621070812923292));
#69278=CARTESIAN_POINT('Ctrl Pts',(2.79949684465664,5.27806149196883,0.464072319581235));
#69279=CARTESIAN_POINT('Ctrl Pts',(5.94469888877439,0.578168532022547,0.307073826239177));
#69280=CARTESIAN_POINT('Ctrl Pts',(3.79743415440745,-4.56550609975241,0.152383053045432));
#69281=CARTESIAN_POINT('Ctrl Pts',(0.216274136307286,-5.31234397836678,
0.0500251109657079));
#69282=CARTESIAN_POINT('Ctrl Pts',(-1.31785621200034,-4.9071451662202,1.74231289118421E-15));
#69283=CARTESIAN_POINT('Origin',(0.,0.,10.2083368446371));
#69284=CARTESIAN_POINT('',(-5.06594495534805,0.00113798286105304,1.79166315536292));
#69285=CARTESIAN_POINT('',(-5.0788676065064,-0.0031096904011537,1.70833684463707));
#69286=CARTESIAN_POINT('',(-5.0736,1.10600941455115E-13,10.2083368446371));
#69287=CARTESIAN_POINT('Ctrl Pts',(-5.0788676065064,-0.00310969040115398,
1.70833684463707));
#69288=CARTESIAN_POINT('Ctrl Pts',(-5.06820560204524,1.46267013662722,1.66221954089824));
#69289=CARTESIAN_POINT('Ctrl Pts',(-3.63653147921883,4.60995381904077,1.56376940604539));
#69290=CARTESIAN_POINT('Ctrl Pts',(1.67938795492248,5.73354207176578,1.41298644007852));
#69291=CARTESIAN_POINT('Ctrl Pts',(5.70869045070874,1.76202618095205,1.25598794673646));
#69292=CARTESIAN_POINT('Ctrl Pts',(4.61877209773216,-3.78910839602635,1.0989894533944));
#69293=CARTESIAN_POINT('Ctrl Pts',(-0.612224753988487,-5.94330155793046,
0.941990960052346));
#69294=CARTESIAN_POINT('Ctrl Pts',(-4.49644008704084,-3.30864398166895,
0.811773423799902));
#69295=CARTESIAN_POINT('Ctrl Pts',(-5.06608310024492,-0.817957632158887,
0.733888718661477));
#69296=CARTESIAN_POINT('Ctrl Pts',(-5.06551066928822,-0.000578487979984235,
0.708336844637072));
#69297=CARTESIAN_POINT('Ctrl Pts',(-5.06594495534805,0.00113798286105242,
1.79166315536292));
#69298=CARTESIAN_POINT('Ctrl Pts',(-5.06751102530523,0.764702257078156,
1.76779552568118));
#69299=CARTESIAN_POINT('Ctrl Pts',(-4.54967353500429,3.20046203254748,1.69159506488542));
#69300=CARTESIAN_POINT('Ctrl Pts',(-0.800856996403053,5.92047503909791,
1.56306177297564));
#69301=CARTESIAN_POINT('Ctrl Pts',(4.49633411524324,3.93401017093414,1.40606327963358));
#69302=CARTESIAN_POINT('Ctrl Pts',(5.76163326143087,-1.58003046734643,1.24906478629152));
#69303=CARTESIAN_POINT('Ctrl Pts',(1.86064021890344,-5.67731097226746,1.09206629294947));
#69304=CARTESIAN_POINT('Ctrl Pts',(-3.54825609197855,-4.71238753324782,
0.939599082639932));
#69305=CARTESIAN_POINT('Ctrl Pts',(-5.07093053185417,-1.51604242073639,
0.839464703444417));
#69306=CARTESIAN_POINT('Ctrl Pts',(-5.0799445016814,0.00237344505285278,
0.791663155362921));
#69307=CARTESIAN_POINT('Origin',(0.,0.,10.2083368446371));
#69308=CARTESIAN_POINT('',(-5.07643096335186,-0.00399326016102722,2.79166315536292));
#69309=CARTESIAN_POINT('',(-5.07274549324388,0.00436695056987321,2.70833684463708));
#69310=CARTESIAN_POINT('',(-5.0736,1.10600941455115E-13,10.2083368446371));
#69311=CARTESIAN_POINT('Ctrl Pts',(-5.07274549324388,0.00436695056987284,
2.70833684463708));
#69312=CARTESIAN_POINT('Ctrl Pts',(-5.07638654156454,0.422701167110148,
2.69521602536304));
#69313=CARTESIAN_POINT('Ctrl Pts',(-4.83926758888069,2.50550600890858,2.62976237497499));
#69314=CARTESIAN_POINT('Ctrl Pts',(-1.97561166336026,5.63828895889383,2.51197589347292));
#69315=CARTESIAN_POINT('Ctrl Pts',(3.6128915810316,4.75818989009414,2.35497740013087));
#69316=CARTESIAN_POINT('Ctrl Pts',(5.96174508817349,-0.388546134793637,
2.19797890678881));
#69317=CARTESIAN_POINT('Ctrl Pts',(2.96474106500057,-5.18686823314646,2.04098041344675));
#69318=CARTESIAN_POINT('Ctrl Pts',(-2.69071315072611,-5.33417912211988,
1.88398192010469));
#69319=CARTESIAN_POINT('Ctrl Pts',(-4.98091385691211,-2.06009093973243,
1.77310073050147));
#69320=CARTESIAN_POINT('Ctrl Pts',(-5.08030459382418,-0.200662320374615,
1.71455237201226));
#69321=CARTESIAN_POINT('Ctrl Pts',(-5.0788676065064,-0.00310969040115398,
1.70833684463707));
#69322=CARTESIAN_POINT('Ctrl Pts',(-5.07643096335186,-0.00399326016102722,
2.79166315536292));
#69323=CARTESIAN_POINT('Ctrl Pts',(-5.06457082001664,1.37091447103077,2.74845917903196));
#69324=CARTESIAN_POINT('Ctrl Pts',(-3.7827320999117,4.43074150154599,2.65292237158698));
#69325=CARTESIAN_POINT('Ctrl Pts',(1.36220151697138,5.81702256793933,2.50505273302799));
#69326=CARTESIAN_POINT('Ctrl Pts',(5.60328669734595,2.07280630409542,2.34805423968593));
#69327=CARTESIAN_POINT('Ctrl Pts',(4.81994564291905,-3.53007932713903,2.19105574634387));
#69328=CARTESIAN_POINT('Ctrl Pts',(-0.285401937658034,-5.96757024490932,
2.03405725300181));
#69329=CARTESIAN_POINT('Ctrl Pts',(-4.39760317314566,-3.49692096558582,
1.90092638934149));
#69330=CARTESIAN_POINT('Ctrl Pts',(-5.0640772165997,-0.90951008575328,1.8201283567952));
#69331=CARTESIAN_POINT('Ctrl Pts',(-5.06594495534805,0.00113798286105242,
1.79166315536292));
#69332=CARTESIAN_POINT('Origin',(0.,0.,10.2083368446371));
#69333=CARTESIAN_POINT('',(-5.07544700173093,0.00419220993169878,3.79166315536292));
#69334=CARTESIAN_POINT('',(-5.06752990436066,-0.00289155559083432,3.70833684463708));
#69335=CARTESIAN_POINT('',(-5.0736,1.10600941455115E-13,10.2083368446371));
#69336=CARTESIAN_POINT('Ctrl Pts',(-5.06752990436066,-0.00289155559083445,
3.70833684463708));
#69337=CARTESIAN_POINT('Ctrl Pts',(-5.06201314247005,1.03465176096834,3.67587967871383));
#69338=CARTESIAN_POINT('Ctrl Pts',(-4.25079971500112,3.75301601020252,3.59108968167655));
#69339=CARTESIAN_POINT('Ctrl Pts',(0.164021032340792,5.97213939901987,3.45396685352527));
#69340=CARTESIAN_POINT('Ctrl Pts',(5.07168429591276,3.15774768001703,3.29696836018321));
#69341=CARTESIAN_POINT('Ctrl Pts',(5.43160651478565,-2.48817267483047,3.13996986684115));
#69342=CARTESIAN_POINT('Ctrl Pts',(0.921047975843499,-5.90296718493849,
2.9829713734991));
#69343=CARTESIAN_POINT('Ctrl Pts',(-3.96942410407231,-4.18159504957827,
2.83909369943107));
#69344=CARTESIAN_POINT('Ctrl Pts',(-5.06186409728241,-1.24583899384963,
2.74754885647706));
#69345=CARTESIAN_POINT('Ctrl Pts',(-5.07274549324388,0.00436695056987284,
2.70833684463708));
#69346=CARTESIAN_POINT('Ctrl Pts',(-5.07544700173093,0.00419220993169878,
3.79166315536292));
#69347=CARTESIAN_POINT('Ctrl Pts',(-5.07831876722643,0.329194847520769,
3.78145566349676));
#69348=CARTESIAN_POINT('Ctrl Pts',(-4.90302280847942,2.31737130051307,3.71891534051658));
#69349=CARTESIAN_POINT('Ctrl Pts',(-2.2821043825461,5.52135344516299,3.60404218642239));
#69350=CARTESIAN_POINT('Ctrl Pts',(3.34628151701835,4.94931755856517,3.44704369308033));
#69351=CARTESIAN_POINT('Ctrl Pts',(5.9740820006751,-0.0607341045204584,
3.29004519973827));
#69352=CARTESIAN_POINT('Ctrl Pts',(3.24496813195078,-5.01632594473331,3.13304670639622));
#69353=CARTESIAN_POINT('Ctrl Pts',(-2.39388416789017,-5.47381611497205,
2.97604821305415));
#69354=CARTESIAN_POINT('Ctrl Pts',(-4.9251294092353,-2.24779066275208,2.86225369604306));
#69355=CARTESIAN_POINT('Ctrl Pts',(-5.0789369717198,-0.294506636106011,
2.80079201014598));
#69356=CARTESIAN_POINT('Ctrl Pts',(-5.07643096335186,-0.00399326016102722,
2.79166315536292));
#69357=CARTESIAN_POINT('Origin',(0.,0.,10.2083368446371));
#69358=CARTESIAN_POINT('',(-5.06623538659821,-0.00165077865025204,4.79166315536292));
#69359=CARTESIAN_POINT('',(-5.08150150384863,-0.000304682560140652,4.70833684463708));
#69360=CARTESIAN_POINT('',(-5.0736,1.10600941455115E-13,10.2083368446371));
#69361=CARTESIAN_POINT('Ctrl Pts',(-5.08150150384863,-0.000304682560140828,
4.70833684463708));
#69362=CARTESIAN_POINT('Ctrl Pts',(-5.08004199361202,1.64362562632391,4.65654333206461));
#69363=CARTESIAN_POINT('Ctrl Pts',(-3.32694734261784,4.95128314317388,4.55241698837811));
#69364=CARTESIAN_POINT('Ctrl Pts',(2.28210462993784,5.52135404368456,4.39595781357762));
#69365=CARTESIAN_POINT('Ctrl Pts',(5.86414511529741,1.14243341683897,4.23895932023555));
#69366=CARTESIAN_POINT('Ctrl Pts',(4.18785084798745,-4.2608986517151,4.0819608268935));
#69367=CARTESIAN_POINT('Ctrl Pts',(-1.24365772802729,-5.8435149929827,3.92496233355144));
#69368=CARTESIAN_POINT('Ctrl Pts',(-4.66764902476596,-2.94237266391977,
3.80042100613263));
#69369=CARTESIAN_POINT('Ctrl Pts',(-5.07090818182747,-0.638247816504467,
3.72821250982785));
#69370=CARTESIAN_POINT('Ctrl Pts',(-5.06752990436066,-0.00289155559083445,
3.70833684463708));
#69371=CARTESIAN_POINT('Ctrl Pts',(-5.06623538659821,-0.00165077865025218,
4.79166315536292));
#69372=CARTESIAN_POINT('Ctrl Pts',(-5.06341382264369,0.943369534950495,
4.76211931684755));
#69373=CARTESIAN_POINT('Ctrl Pts',(-4.35931582912874,3.56626810599387,4.68024264721815));
#69374=CARTESIAN_POINT('Ctrl Pts',(-0.164021014606317,5.97213875156532,
4.54603314647473));
#69375=CARTESIAN_POINT('Ctrl Pts',(4.89071815558305,3.43135837605058,4.38903465313268));
#69376=CARTESIAN_POINT('Ctrl Pts',(5.55998718173337,-2.18629522837624,4.23203615979062));
#69377=CARTESIAN_POINT('Ctrl Pts',(1.24365759322077,-5.84351435953346,4.07503766644856));
#69378=CARTESIAN_POINT('Ctrl Pts',(-3.83471277836695,-4.36379434722342,
3.92824666497267));
#69379=CARTESIAN_POINT('Ctrl Pts',(-5.06359550115425,-1.33706248264138,
3.83378849461079));
#69380=CARTESIAN_POINT('Ctrl Pts',(-5.07544700173093,0.00419220993169878,
3.79166315536292));
#69381=CARTESIAN_POINT('Origin',(0.,0.,10.2083368446371));
#69382=CARTESIAN_POINT('',(-5.08061550220448,-0.00187835596255306,5.79166315536292));
#69383=CARTESIAN_POINT('',(-5.06818254924878,0.00327741817492065,5.70833684463708));
#69384=CARTESIAN_POINT('',(-5.0736,1.10600941455115E-13,10.2083368446371));
#69385=CARTESIAN_POINT('Ctrl Pts',(-5.06818254924878,0.00327741817492046,
5.70833684463708));
#69386=CARTESIAN_POINT('Ctrl Pts',(-5.07183456953104,0.603958443996534,
5.68953981652941));
#69387=CARTESIAN_POINT('Ctrl Pts',(-4.69736642816282,2.87259326592426,5.61840995730772));
#69388=CARTESIAN_POINT('Ctrl Pts',(-1.36220166545199,5.81702319809857,5.49494726697201));
#69389=CARTESIAN_POINT('Ctrl Pts',(4.10035928902097,4.34515876133492,5.33794877362997));
#69390=CARTESIAN_POINT('Ctrl Pts',(5.88615929841981,-1.02297668832719,5.1809502802879));
#69391=CARTESIAN_POINT('Ctrl Pts',(2.3938844275315,-5.47381670826519,5.02395178694585));
#69392=CARTESIAN_POINT('Ctrl Pts',(-3.24496848378481,-5.01632648853908,
4.86695329360378));
#69393=CARTESIAN_POINT('Ctrl Pts',(-5.07375293308448,-1.69557487064781,
4.7617483128342));
#69394=CARTESIAN_POINT('Ctrl Pts',(-5.08151670152288,-0.0174226970094883,
4.70887616317863));
#69395=CARTESIAN_POINT('Ctrl Pts',(-5.08150150384863,-0.000304682560140828,
4.70833684463708));
#69396=CARTESIAN_POINT('Ctrl Pts',(-5.08061550220448,-0.00187835596255308,
5.79166315536293));
#69397=CARTESIAN_POINT('Ctrl Pts',(-5.07313315332044,1.5503069404754,5.74278297019833));
#69398=CARTESIAN_POINT('Ctrl Pts',(-3.48999114796195,4.77754415127511,5.64156995391971));
#69399=CARTESIAN_POINT('Ctrl Pts',(1.97561144788205,5.63828834519714,5.48802410652708));
#69400=CARTESIAN_POINT('Ctrl Pts',(5.79259970947732,1.46257867915377,5.33102561318502));
#69401=CARTESIAN_POINT('Ctrl Pts',(4.41540665009831,-4.0246153410012,5.17402711984296));
#69402=CARTESIAN_POINT('Ctrl Pts',(-0.92104787574744,-5.90296654461282,
5.01702862650091));
#69403=CARTESIAN_POINT('Ctrl Pts',(-4.58281307585404,-3.13076536575022,
4.88957397167423));
#69404=CARTESIAN_POINT('Ctrl Pts',(-5.0684118336446,-0.730603481292581,
4.81445214796157));
#69405=CARTESIAN_POINT('Ctrl Pts',(-5.06623538659821,-0.00165077865025218,
4.79166315536292));
#69406=CARTESIAN_POINT('Origin',(0.,0.,10.2083368446371));
#69407=CARTESIAN_POINT('',(-5.07032350272244,0.00406483722298734,6.79166315536293));
#69408=CARTESIAN_POINT('',(-5.07176207912418,-0.00429478512726797,6.70833684463708));
#69409=CARTESIAN_POINT('',(-5.0736,1.10600941455115E-13,10.2083368446371));
#69410=CARTESIAN_POINT('Ctrl Pts',(-5.07176207912418,-0.00429478512726802,
6.70833684463708));
#69411=CARTESIAN_POINT('Ctrl Pts',(-5.06152064599786,1.21211560888524,6.67020346988019));
#69412=CARTESIAN_POINT('Ctrl Pts',(-4.01723926286446,4.11367300543969,6.57973726400929));
#69413=CARTESIAN_POINT('Ctrl Pts',(0.800857062853464,5.92047566764934,6.43693822702436));
#69414=CARTESIAN_POINT('Ctrl Pts',(5.37989341709942,2.59808361512381,6.27993973368231));
#69415=CARTESIAN_POINT('Ctrl Pts',(5.13483694964473,-3.0539846259906,6.12294124034024));
#69416=CARTESIAN_POINT('Ctrl Pts',(0.285401972927619,-5.96757088942664,
5.96594274699819));
#69417=CARTESIAN_POINT('Ctrl Pts',(-4.20869589117159,-3.8219142963774,5.8277412817638));
#69418=CARTESIAN_POINT('Ctrl Pts',(-5.06166697497504,-1.0683984039935,5.74187264764343));
#69419=CARTESIAN_POINT('Ctrl Pts',(-5.06818254924878,0.00327741817492046,
5.70833684463708));
#69420=CARTESIAN_POINT('Ctrl Pts',(-5.07032350272244,0.00406483722298713,
6.79166315536293));
#69421=CARTESIAN_POINT('Ctrl Pts',(-5.07426970367213,0.511087407033013,
6.77577945466313));
#69422=CARTESIAN_POINT('Ctrl Pts',(-4.77323782375589,2.68406204063008,6.70756292284932));
#69423=CARTESIAN_POINT('Ctrl Pts',(-1.67938775292856,5.73354154736347,6.58701355992148));
#69424=CARTESIAN_POINT('Ctrl Pts',(3.85566217988192,4.56363706615652,6.43001506657943));
#69425=CARTESIAN_POINT('Ctrl Pts',(5.93344523009267,-0.69834389981148,6.27301657323736));
#69426=CARTESIAN_POINT('Ctrl Pts',(2.69071284975304,-5.33417856632519,6.11601807989532));
#69427=CARTESIAN_POINT('Ctrl Pts',(-2.96474073765194,-5.18686765769478,
5.95901958655325));
#69428=CARTESIAN_POINT('Ctrl Pts',(-5.0286520759667,-1.88246391579033,5.85090127837579));
#69429=CARTESIAN_POINT('Ctrl Pts',(-5.08114401701022,-0.111516776080137,
5.79511580131235));
#69430=CARTESIAN_POINT('Ctrl Pts',(-5.08061550220448,-0.00187835596255308,
5.79166315536293));
#69431=CARTESIAN_POINT('Origin',(0.,0.,10.2083368446371));
#69432=CARTESIAN_POINT('',(-5.0667809979009,-0.000656412822606089,7.79166315536293));
#69433=CARTESIAN_POINT('',(-5.07934275226421,0.00276793540382957,7.70833684463708));
#69434=CARTESIAN_POINT('',(-5.0736,1.10600941455115E-13,10.2083368446371));
#69435=CARTESIAN_POINT('',(-1.31303618635646,-4.90075024188322,8.));
#69436=CARTESIAN_POINT('Ctrl Pts',(-1.31303618635644,-4.90075024188323,
8.));
#69437=CARTESIAN_POINT('Ctrl Pts',(-2.11876087752226,-4.68487601374973,
7.97383358444299));
#69438=CARTESIAN_POINT('Ctrl Pts',(-3.61103600209076,-3.84612122823184,
7.92150075332897));
#69439=CARTESIAN_POINT('Ctrl Pts',(-4.8640953672922,-1.92805050100101,7.85205513844995));
#69440=CARTESIAN_POINT('Ctrl Pts',(-5.07037793642002,-0.54712311490011,
7.80877593912793));
#69441=CARTESIAN_POINT('Ctrl Pts',(-5.0667809979009,-0.000656412822605951,
7.79166315536293));
#69442=CARTESIAN_POINT('',(1.31785785677863,-4.90714579947409,8.00000000000001));
#69443=CARTESIAN_POINT('Origin',(0.,0.,8.));
#69444=CARTESIAN_POINT('Ctrl Pts',(1.31785785677863,-4.90714579947409,8.00000000000001));
#69445=CARTESIAN_POINT('Ctrl Pts',(-0.216269591468087,-5.31234554625424,
7.9499748890343));
#69446=CARTESIAN_POINT('Ctrl Pts',(-3.61771514871704,-4.60298607712906,
7.85275383724664));
#69447=CARTESIAN_POINT('Ctrl Pts',(-5.07021586478366,-1.49689387689792,
7.75553278545901));
#69448=CARTESIAN_POINT('Ctrl Pts',(-5.07934275226421,0.00276793540382986,
7.70833684463708));
#69449=CARTESIAN_POINT('Origin',(0.,0.,10.2083368446371));
#69450=CARTESIAN_POINT('Ctrl Pts',(-5.07934275226421,0.00276793540383012,
7.70833684463708));
#69451=CARTESIAN_POINT('Ctrl Pts',(-5.08033613895975,0.165993799129837,
7.70319995434499));
#69452=CARTESIAN_POINT('Ctrl Pts',(-4.99920696262547,1.99102187228673,7.64573023293889));
#69453=CARTESIAN_POINT('Ctrl Pts',(-2.799497488489,5.27806255262917,7.53592768041876));
#69454=CARTESIAN_POINT('Ctrl Pts',(2.8591428156985,5.24623244979999,7.37892918707671));
#69455=CARTESIAN_POINT('Ctrl Pts',(5.95237094349663,0.509586379962791,7.22193069373465));
#69456=CARTESIAN_POINT('Ctrl Pts',(3.70900729550924,-4.68371090122276,7.06493220039259));
#69457=CARTESIAN_POINT('Ctrl Pts',(-1.86064034918539,-5.67731151891722,
6.90793370705054));
#69458=CARTESIAN_POINT('Ctrl Pts',(-4.81412133745352,-2.5752195014975,6.78906858846536));
#69459=CARTESIAN_POINT('Ctrl Pts',(-5.07557560949328,-0.457240961862529,
6.72253630099421));
#69460=CARTESIAN_POINT('Ctrl Pts',(-5.07176207912418,-0.00429478512726802,
6.70833684463708));
#69461=CARTESIAN_POINT('Ctrl Pts',(-5.0667809979009,-0.000656412822605951,
7.79166315536293));
#69462=CARTESIAN_POINT('Ctrl Pts',(-5.05937809100424,1.12403395819613,7.75644310801391));
#69463=CARTESIAN_POINT('Ctrl Pts',(-4.14423912611421,3.92453560182124,7.66889022955088));
#69464=CARTESIAN_POINT('Ctrl Pts',(0.476758320675261,5.95830042580594,7.52900451997384));
#69465=CARTESIAN_POINT('Ctrl Pts',(5.22810884028568,2.88800998678043,7.37200602663177));
#69466=CARTESIAN_POINT('Ctrl Pts',(5.29527916712856,-2.76679132542031,7.21500753328971));
#69467=CARTESIAN_POINT('Ctrl Pts',(0.612224870220684,-5.9433011663707,7.05800903994766));
#69468=CARTESIAN_POINT('Ctrl Pts',(-4.08954628424525,-4.00704976176015,
6.91689424730539));
#69469=CARTESIAN_POINT('Ctrl Pts',(-5.0612679560476,-1.15942546766541,6.82811228577715));
#69470=CARTESIAN_POINT('Ctrl Pts',(-5.07032350272244,0.00406483722298713,
6.79166315536293));
#69471=CARTESIAN_POINT('Ctrl Pts',(3.43378788736183,2.93584158413004,8.));
#69472=CARTESIAN_POINT('Ctrl Pts',(3.91646501574697,2.37129788193754,7.97383358444299));
#69473=CARTESIAN_POINT('Ctrl Pts',(4.58922505888624,1.00348867934585,7.92150075332897));
#69474=CARTESIAN_POINT('Ctrl Pts',(4.5186273771248,-2.07044295135642,7.81683509110093));
#69475=CARTESIAN_POINT('Ctrl Pts',(1.60472354186206,-5.07186039848098,7.68600301331589));
#69476=CARTESIAN_POINT('Ctrl Pts',(-3.35287702678038,-4.13364886539305,
7.52900451997383));
#69477=CARTESIAN_POINT('Ctrl Pts',(-5.29341307506948,0.514825336495039,
7.37200602663177));
#69478=CARTESIAN_POINT('Ctrl Pts',(-2.49279205665034,4.69981218407846,7.21500753328972));
#69479=CARTESIAN_POINT('Ctrl Pts',(2.5459028018807,4.67146930189292,7.05800903994766));
#69480=CARTESIAN_POINT('Ctrl Pts',(5.3002451572812,0.453757463748993,6.90101054660559));
#69481=CARTESIAN_POINT('Ctrl Pts',(3.30265841006127,-4.17057610454098,6.74401205326355));
#69482=CARTESIAN_POINT('Ctrl Pts',(-1.6567935859217,-5.05532050508283,6.58701355992147));
#69483=CARTESIAN_POINT('Ctrl Pts',(-5.13040478426442,-1.40692675790748,
6.43001506657944));
#69484=CARTESIAN_POINT('Ctrl Pts',(-4.00372822142153,3.50301097463029,6.27301657323735));
#69485=CARTESIAN_POINT('Ctrl Pts',(0.713117312304132,5.27184424225852,6.11601807989532));
#69486=CARTESIAN_POINT('Ctrl Pts',(4.79048673232043,2.31344454671744,5.95901958655324));
#69487=CARTESIAN_POINT('Ctrl Pts',(4.57227799378301,-2.71939826633338,5.8020210932112));
#69488=CARTESIAN_POINT('Ctrl Pts',(0.254134098705802,-5.31377983792714,
5.64502259986913));
#69489=CARTESIAN_POINT('Ctrl Pts',(-4.2918858010234,-3.14333365162852,5.48802410652709));
#69490=CARTESIAN_POINT('Ctrl Pts',(-4.98940618387219,1.8457154089275,5.33102561318501));
#69491=CARTESIAN_POINT('Ctrl Pts',(-1.21296250672023,5.17972574763675,5.17402711984298));
#69492=CARTESIAN_POINT('Ctrl Pts',(3.65113492943364,3.86911482852823,5.0170286265009));
#69493=CARTESIAN_POINT('Ctrl Pts',(5.24128748234707,-0.910902107712505,
4.86003013315885));
#69494=CARTESIAN_POINT('Ctrl Pts',(2.13161687410921,-4.87412003976763,4.70303163981679));
#69495=CARTESIAN_POINT('Ctrl Pts',(-2.88945844521027,-4.46675122075005,
4.54603314647474));
#69496=CARTESIAN_POINT('Ctrl Pts',(-5.31957818590282,-0.0540802448651307,
4.38903465313267));
#69497=CARTESIAN_POINT('Ctrl Pts',(-2.97967221743332,4.40708408702865,4.23203615979062));
#69498=CARTESIAN_POINT('Ctrl Pts',(2.0320833711569,4.91644931229421,4.07503766644856));
#69499=CARTESIAN_POINT('Ctrl Pts',(5.22168511404818,1.01727147763408,3.9180391731065));
#69500=CARTESIAN_POINT('Ctrl Pts',(3.7290411480005,-3.79408603038985,3.76104067976445));
#69501=CARTESIAN_POINT('Ctrl Pts',(-1.10740592494388,-5.20331517256929,
3.60404218642238));
#69502=CARTESIAN_POINT('Ctrl Pts',(-4.95085044410053,-1.94677080151586,
3.44704369308033));
#69503=CARTESIAN_POINT('Ctrl Pts',(-4.35490467170682,3.05542829226346,3.29004519973827));
#69504=CARTESIAN_POINT('Ctrl Pts',(0.146051328220124,5.31784783386984,3.13304670639621));
#69505=CARTESIAN_POINT('Ctrl Pts',(4.51604417531138,2.81179331862917,2.97604821305416));
#69506=CARTESIAN_POINT('Ctrl Pts',(4.83653428180639,-2.21557515407508,2.8190497197121));
#69507=CARTESIAN_POINT('Ctrl Pts',(0.820140431422849,-5.25625394192603,
2.66205122637004));
#69508=CARTESIAN_POINT('Ctrl Pts',(-3.93166697371103,-3.58368967284698,
2.50505273302798));
#69509=CARTESIAN_POINT('Ctrl Pts',(-5.15797858932007,1.30234262409331,2.34805423968593));
#69510=CARTESIAN_POINT('Ctrl Pts',(-1.75916895146362,5.02057315201092,2.19105574634387));
#69511=CARTESIAN_POINT('Ctrl Pts',(3.21707287531645,4.23689537527058,2.03405725300181));
#69512=CARTESIAN_POINT('Ctrl Pts',(5.30859229582462,-0.345978063005356,
1.87705875965975));
#69513=CARTESIAN_POINT('Ctrl Pts',(2.63993199038283,-4.61860886950043,1.7200602663177));
#69514=CARTESIAN_POINT('Ctrl Pts',(-2.39592583898866,-4.74978077281557,
1.56306177297564));
#69515=CARTESIAN_POINT('Ctrl Pts',(-5.28339345476216,-0.621835317076693,
1.40606327963358));
#69516=CARTESIAN_POINT('Ctrl Pts',(-3.43324656738056,4.06365773166108,1.24906478629152));
#69517=CARTESIAN_POINT('Ctrl Pts',(1.4953987175479,5.10539058946701,1.09206629294947));
#69518=CARTESIAN_POINT('Ctrl Pts',(5.08326164531879,1.56898332130955,0.935067799607405));
#69519=CARTESIAN_POINT('Ctrl Pts',(4.1127518220848,-3.37398384897273,0.778069306265351));
#69520=CARTESIAN_POINT('Ctrl Pts',(-0.545151052966628,-5.29216938925817,
0.621070812923291));
#69521=CARTESIAN_POINT('Ctrl Pts',(-4.71514359968435,-2.4636695471729,0.464072319581234));
#69522=CARTESIAN_POINT('Ctrl Pts',(-4.65533046585126,2.57160754473359,0.307073826239176));
#69523=CARTESIAN_POINT('Ctrl Pts',(-0.424529207286798,5.30552657624457,
0.150075332897118));
#69524=CARTESIAN_POINT('Ctrl Pts',(4.1935876756527,3.27303039309136,-0.00692316044493899));
#69525=CARTESIAN_POINT('Ctrl Pts',(4.89705802532881,-0.850617472596149,
-0.137755238229987));
#69526=CARTESIAN_POINT('Ctrl Pts',(3.21543569039412,-3.42475539150235,-0.242420900458027));
#69527=CARTESIAN_POINT('Ctrl Pts',(1.88663512189109,-4.17161357046627,-0.294753731572044));
#69528=CARTESIAN_POINT('Ctrl Pts',(1.16918346556927,-4.36383719750628,-0.320920147129053));
#69529=CARTESIAN_POINT('Ctrl Pts',(3.574615437742,3.05624720968396,8.10697338237635));
#69530=CARTESIAN_POINT('Ctrl Pts',(4.0770882669231,2.46855026993857,8.08080696681934));
#69531=CARTESIAN_POINT('Ctrl Pts',(4.77743974901458,1.04464406144345,8.02847413570532));
#69532=CARTESIAN_POINT('Ctrl Pts',(4.7039466937149,-2.15535658568851,7.92380847347729));
#69533=CARTESIAN_POINT('Ctrl Pts',(1.67053695050899,-5.27986907555073,7.79297639569223));
#69534=CARTESIAN_POINT('Ctrl Pts',(-3.49038623640434,-4.30317932648753,
7.63597790235018));
#69535=CARTESIAN_POINT('Ctrl Pts',(-5.51050813771329,0.535939509353267,
7.47897940900812));
#69536=CARTESIAN_POINT('Ctrl Pts',(-2.59502720059656,4.8925623069287,7.32198091566607));
#69537=CARTESIAN_POINT('Ctrl Pts',(2.65031613981997,4.86305701786194,7.16498242232401));
#69538=CARTESIAN_POINT('Ctrl Pts',(5.51762041935301,0.472367102486928,7.00798392898195));
#69539=CARTESIAN_POINT('Ctrl Pts',(3.43810803854393,-4.34162103676824,6.85098543563989));
#69540=CARTESIAN_POINT('Ctrl Pts',(-1.72474250700959,-5.26265084302763,
6.69398694229783));
#69541=CARTESIAN_POINT('Ctrl Pts',(-5.34081450144173,-1.46462806485474,
6.53698844895577));
#69542=CARTESIAN_POINT('Ctrl Pts',(-4.16793033765764,3.64667752326241,6.37998995561372));
#69543=CARTESIAN_POINT('Ctrl Pts',(0.742363895820577,5.48805471738879,6.22299146227166));
#69544=CARTESIAN_POINT('Ctrl Pts',(4.98695562724675,2.40832423618623,6.0659929689296));
#69545=CARTESIAN_POINT('Ctrl Pts',(4.75979764573692,-2.83092705288579,5.90899447558755));
#69546=CARTESIAN_POINT('Ctrl Pts',(0.264556723446406,-5.53171018842698,
5.75199598224549));
#69547=CARTESIAN_POINT('Ctrl Pts',(-4.4679059233187,-3.27224900479161,5.59499748890343));
#69548=CARTESIAN_POINT('Ctrl Pts',(-5.19403322368223,1.92141244912467,5.43799899556137));
#69549=CARTESIAN_POINT('Ctrl Pts',(-1.26270889296415,5.39215823112403,5.28100050221931));
#69550=CARTESIAN_POINT('Ctrl Pts',(3.80087638262942,4.02779613946379,5.12400200887726));
#69551=CARTESIAN_POINT('Ctrl Pts',(5.45624475437132,-0.948260301250735,
4.96700351553519));
#69552=CARTESIAN_POINT('Ctrl Pts',(2.21903939191664,-5.07401892926682,4.81000502219315));
#69553=CARTESIAN_POINT('Ctrl Pts',(-3.00796179140179,-4.64994297667973,
4.65300652885108));
#69554=CARTESIAN_POINT('Ctrl Pts',(-5.53774634000859,-0.05629820027127,
4.49600803550903));
#69555=CARTESIAN_POINT('Ctrl Pts',(-3.10187543821507,4.58782875637178,4.33900954216697));
#69556=CARTESIAN_POINT('Ctrl Pts',(2.11542379075055,5.11808422275766,4.18201104882491));
#69557=CARTESIAN_POINT('Ctrl Pts',(5.43583844779792,1.05899212403571,4.02501255548285));
#69558=CARTESIAN_POINT('Ctrl Pts',(3.88197771466281,-3.94969023749826,3.8680140621408));
#69559=CARTESIAN_POINT('Ctrl Pts',(-1.15282319263835,-5.4167151127071,3.71101556879874));
#69560=CARTESIAN_POINT('Ctrl Pts',(-5.15389622421624,-2.0266123561262,3.55401707545668));
#69561=CARTESIAN_POINT('Ctrl Pts',(-4.53350934304161,3.18073844416463,3.39701858211462));
#69562=CARTESIAN_POINT('Ctrl Pts',(0.152041229593681,5.53594502225318,3.24002008877256));
#69563=CARTESIAN_POINT('Ctrl Pts',(4.70125754884517,2.92711143909179,3.08302159543051));
#69564=CARTESIAN_POINT('Ctrl Pts',(5.03489169279947,-2.30644099432688,2.92602310208845));
#69565=CARTESIAN_POINT('Ctrl Pts',(0.853776279563064,-5.47182502293018,
2.7690246087464));
#69566=CARTESIAN_POINT('Ctrl Pts',(-4.09291369219827,-3.730665040722,2.61202611540433));
#69567=CARTESIAN_POINT('Ctrl Pts',(-5.36951917175407,1.3557546948219,2.45502762206228));
#69568=CARTESIAN_POINT('Ctrl Pts',(-1.83131652209583,5.22647842097189,2.29802912872022));
#69569=CARTESIAN_POINT('Ctrl Pts',(3.34901244388816,4.41066021354511,2.14103063537816));
#69570=CARTESIAN_POINT('Ctrl Pts',(5.52630989327424,-0.360167420268118,
1.9840321420361));
#69571=CARTESIAN_POINT('Ctrl Pts',(2.74820168192207,-4.80802865738244,1.82703364869405));
#69572=CARTESIAN_POINT('Ctrl Pts',(-2.49418827623448,-4.94458022258368,
1.67003515535199));
#69573=CARTESIAN_POINT('Ctrl Pts',(-5.50007758969876,-0.647338215717022,
1.51303666200993));
#69574=CARTESIAN_POINT('Ctrl Pts',(-3.57405191698147,4.23031769514908,1.35603816866787));
#69575=CARTESIAN_POINT('Ctrl Pts',(1.55672846333943,5.31477441689994,1.19903967532582));
#69576=CARTESIAN_POINT('Ctrl Pts',(5.2917379137821,1.63333094119038,1.04204118198376));
#69577=CARTESIAN_POINT('Ctrl Pts',(4.28142524730059,-3.5123586979906,0.885042688641701));
#69578=CARTESIAN_POINT('Ctrl Pts',(-0.567508953307252,-5.50921344548227,
0.728044195299643));
#69579=CARTESIAN_POINT('Ctrl Pts',(-4.90852249920177,-2.56471030992692,
0.571045701957585));
#69580=CARTESIAN_POINT('Ctrl Pts',(-4.84625629098129,2.67707509338356,0.414047208615528));
#69581=CARTESIAN_POINT('Ctrl Pts',(-0.441940127905122,5.52311844147288,
0.257048715273468));
#69582=CARTESIAN_POINT('Ctrl Pts',(4.3655763654143,3.40726490835521,0.100050221931412));
#69583=CARTESIAN_POINT('Ctrl Pts',(5.09789765444943,-0.885503254393324,
-0.0307818558536364));
#69584=CARTESIAN_POINT('Ctrl Pts',(3.3473081142412,-3.56521249842258,-0.135447518081676));
#69585=CARTESIAN_POINT('Ctrl Pts',(1.96401037376818,-4.34270105156074,-0.187780349195693));
#69586=CARTESIAN_POINT('Ctrl Pts',(1.21713437249836,-4.54280821229859,-0.213946764752702));
#69587=CARTESIAN_POINT('Ctrl Pts',(3.71544298812217,3.17665283523789,8.21394676475271));
#69588=CARTESIAN_POINT('Ctrl Pts',(4.23771151809924,2.5658026579396,8.1877803491957));
#69589=CARTESIAN_POINT('Ctrl Pts',(4.96565443914292,1.08579944354106,8.13544751808168));
#69590=CARTESIAN_POINT('Ctrl Pts',(4.889266010305,-2.24027022002061,8.03078185585363));
#69591=CARTESIAN_POINT('Ctrl Pts',(1.73635035915592,-5.48787775262049,7.89994977806859));
#69592=CARTESIAN_POINT('Ctrl Pts',(-3.62789544602829,-4.472709787582,7.74295128472654));
#69593=CARTESIAN_POINT('Ctrl Pts',(-5.72760320035712,0.557053682211493,
7.58595279138447));
#69594=CARTESIAN_POINT('Ctrl Pts',(-2.69726234454278,5.08531242977894,7.42895429804241));
#69595=CARTESIAN_POINT('Ctrl Pts',(2.75472947775923,5.05464473383097,7.27195580470038));
#69596=CARTESIAN_POINT('Ctrl Pts',(5.73499568142482,0.490976741224864,7.11495731135828));
#69597=CARTESIAN_POINT('Ctrl Pts',(3.57355766702658,-4.5126659689955,6.95795881801627));
#69598=CARTESIAN_POINT('Ctrl Pts',(-1.7926914280975,-5.46998118097242,6.80096032467417));
#69599=CARTESIAN_POINT('Ctrl Pts',(-5.55122421861904,-1.522329371802,6.64396183133214));
#69600=CARTESIAN_POINT('Ctrl Pts',(-4.33213245389376,3.79034407189453,6.48696333799006));
#69601=CARTESIAN_POINT('Ctrl Pts',(0.771610479337022,5.70426519251906,6.32996484464802));
#69602=CARTESIAN_POINT('Ctrl Pts',(5.18342452217309,2.50320392565502,6.17296635130595));
#69603=CARTESIAN_POINT('Ctrl Pts',(4.94731729769082,-2.9424558394382,6.01596785796391));
#69604=CARTESIAN_POINT('Ctrl Pts',(0.274979348187014,-5.7496405389268,5.85896936462183));
#69605=CARTESIAN_POINT('Ctrl Pts',(-4.64392604561401,-3.40116435795471,
5.70197087127979));
#69606=CARTESIAN_POINT('Ctrl Pts',(-5.39866026349227,1.99710948932185,5.54497237793772));
#69607=CARTESIAN_POINT('Ctrl Pts',(-1.31245527920807,5.6045907146113,5.38797388459567));
#69608=CARTESIAN_POINT('Ctrl Pts',(3.95061783582519,4.18647745039935,5.23097539125361));
#69609=CARTESIAN_POINT('Ctrl Pts',(5.67120202639557,-0.985618494788963,
5.07397689791155));
#69610=CARTESIAN_POINT('Ctrl Pts',(2.30646190972407,-5.273917818766,4.9169784045695));
#69611=CARTESIAN_POINT('Ctrl Pts',(-3.1264651375933,-4.83313473260941,4.75997991122743));
#69612=CARTESIAN_POINT('Ctrl Pts',(-5.75591449411437,-0.058516155677411,
4.60298141788538));
#69613=CARTESIAN_POINT('Ctrl Pts',(-3.22407865899683,4.76857342571492,4.44598292454332));
#69614=CARTESIAN_POINT('Ctrl Pts',(2.19876421034419,5.31971913322111,4.28898443120126));
#69615=CARTESIAN_POINT('Ctrl Pts',(5.64999178154766,1.10071277043733,4.1319859378592));
#69616=CARTESIAN_POINT('Ctrl Pts',(4.03491428132513,-4.10529444460668,3.97498744451715));
#69617=CARTESIAN_POINT('Ctrl Pts',(-1.19824046033282,-5.6301150528449,3.81798895117509));
#69618=CARTESIAN_POINT('Ctrl Pts',(-5.35694200433196,-2.10645391073654,
3.66099045783303));
#69619=CARTESIAN_POINT('Ctrl Pts',(-4.7121140143764,3.30604859606581,3.50399196449097));
#69620=CARTESIAN_POINT('Ctrl Pts',(0.158031130967237,5.75404221063653,3.34699347114891));
#69621=CARTESIAN_POINT('Ctrl Pts',(4.88647092237896,3.04242955955441,3.18999497780686));
#69622=CARTESIAN_POINT('Ctrl Pts',(5.23324910379256,-2.39730683457867,3.0329964844648));
#69623=CARTESIAN_POINT('Ctrl Pts',(0.887412127703281,-5.68739610393434,
2.87599799112275));
#69624=CARTESIAN_POINT('Ctrl Pts',(-4.25416041068552,-3.87764040859701,
2.71899949778068));
#69625=CARTESIAN_POINT('Ctrl Pts',(-5.58105975418807,1.40916676555049,2.56200100443863));
#69626=CARTESIAN_POINT('Ctrl Pts',(-1.90346409272805,5.43238368993286,2.40500251109657));
#69627=CARTESIAN_POINT('Ctrl Pts',(3.48095201245988,4.58442505181962,2.24800401775452));
#69628=CARTESIAN_POINT('Ctrl Pts',(5.74402749072386,-0.374356777530876,
2.09100552441245));
#69629=CARTESIAN_POINT('Ctrl Pts',(2.85647137346132,-4.99744844526445,1.9340070310704));
#69630=CARTESIAN_POINT('Ctrl Pts',(-2.5924507134803,-5.13937967235178,1.77700853772834));
#69631=CARTESIAN_POINT('Ctrl Pts',(-5.71676172463537,-0.672841114357358,
1.62001004438628));
#69632=CARTESIAN_POINT('Ctrl Pts',(-3.71485726658238,4.39697765863709,1.46301155104423));
#69633=CARTESIAN_POINT('Ctrl Pts',(1.61805820913096,5.52415824433286,1.30601305770217));
#69634=CARTESIAN_POINT('Ctrl Pts',(5.50021418224542,1.69767856107122,1.14901456436011));
#69635=CARTESIAN_POINT('Ctrl Pts',(4.45009867251637,-3.65073354700848,0.992016071018051));
#69636=CARTESIAN_POINT('Ctrl Pts',(-0.589866853647869,-5.72625750170636,
0.835017577675995));
#69637=CARTESIAN_POINT('Ctrl Pts',(-5.1019013987192,-2.66575107268096,0.678019084333936));
#69638=CARTESIAN_POINT('Ctrl Pts',(-5.0371821161113,2.78254264203352,0.521020590991878));
#69639=CARTESIAN_POINT('Ctrl Pts',(-0.459351048523452,5.74071030670118,
0.36402209764982));
#69640=CARTESIAN_POINT('Ctrl Pts',(4.53756505517591,3.54149942361907,0.207023604307763));
#69641=CARTESIAN_POINT('Ctrl Pts',(5.29873728357006,-0.920389036190499,
0.076191526522715));
#69642=CARTESIAN_POINT('Ctrl Pts',(3.47918053808829,-3.70566960534281,-0.0284741357053249));
#69643=CARTESIAN_POINT('Ctrl Pts',(2.04138562564527,-4.51378853265522,-0.0808069668193416));
#69644=CARTESIAN_POINT('Ctrl Pts',(1.26508527942745,-4.7217792270909,-0.106973382376351));
#69645=CARTESIAN_POINT('Ctrl Pts',(3.85627053850235,3.29705846079181,8.32092014712906));
#69646=CARTESIAN_POINT('Ctrl Pts',(4.39833476927537,2.66305504594064,8.29475373157205));
#69647=CARTESIAN_POINT('Ctrl Pts',(5.15386912927126,1.12695482563867,8.24242090045804));
#69648=CARTESIAN_POINT('Ctrl Pts',(5.0745853268951,-2.3251838543527,8.13775523822997));
#69649=CARTESIAN_POINT('Ctrl Pts',(1.80216376780286,-5.69588642969024,8.00692316044496));
#69650=CARTESIAN_POINT('Ctrl Pts',(-3.76540465565226,-4.64224024867649,
7.84992466710287));
#69651=CARTESIAN_POINT('Ctrl Pts',(-5.94469826300093,0.578167855069724,
7.69292617376083));
#69652=CARTESIAN_POINT('Ctrl Pts',(-2.799497488489,5.27806255262917,7.53592768041876));
#69653=CARTESIAN_POINT('Ctrl Pts',(2.8591428156985,5.24623244979999,7.37892918707671));
#69654=CARTESIAN_POINT('Ctrl Pts',(5.95237094349663,0.509586379962791,7.22193069373465));
#69655=CARTESIAN_POINT('Ctrl Pts',(3.70900729550924,-4.68371090122276,7.06493220039259));
#69656=CARTESIAN_POINT('Ctrl Pts',(-1.86064034918539,-5.67731151891722,
6.90793370705054));
#69657=CARTESIAN_POINT('Ctrl Pts',(-5.76163393579635,-1.58003067874924,
6.75093521370848));
#69658=CARTESIAN_POINT('Ctrl Pts',(-4.49633457012987,3.93401062052664,6.59393672036642));
#69659=CARTESIAN_POINT('Ctrl Pts',(0.800857062853464,5.92047566764934,6.43693822702436));
#69660=CARTESIAN_POINT('Ctrl Pts',(5.37989341709942,2.59808361512381,6.27993973368231));
#69661=CARTESIAN_POINT('Ctrl Pts',(5.13483694964473,-3.0539846259906,6.12294124034024));
#69662=CARTESIAN_POINT('Ctrl Pts',(0.285401972927619,-5.96757088942664,
5.96594274699819));
#69663=CARTESIAN_POINT('Ctrl Pts',(-4.81994616790931,-3.5300797111178,5.80894425365613));
#69664=CARTESIAN_POINT('Ctrl Pts',(-5.6032873033023,2.07280652951902,5.65194576031408));
#69665=CARTESIAN_POINT('Ctrl Pts',(-1.36220166545199,5.81702319809857,5.49494726697201));
#69666=CARTESIAN_POINT('Ctrl Pts',(4.10035928902097,4.34515876133492,5.33794877362997));
#69667=CARTESIAN_POINT('Ctrl Pts',(5.88615929841981,-1.02297668832719,5.1809502802879));
#69668=CARTESIAN_POINT('Ctrl Pts',(2.3938844275315,-5.47381670826519,5.02395178694585));
#69669=CARTESIAN_POINT('Ctrl Pts',(-3.24496848378481,-5.01632648853908,
4.86695329360378));
#69670=CARTESIAN_POINT('Ctrl Pts',(-5.97408264822014,-0.0607341110835563,
4.70995480026174));
#69671=CARTESIAN_POINT('Ctrl Pts',(-3.34628187977858,4.94931809505806,4.55295630691966));
#69672=CARTESIAN_POINT('Ctrl Pts',(2.28210462993784,5.52135404368456,4.39595781357762));
#69673=CARTESIAN_POINT('Ctrl Pts',(5.86414511529741,1.14243341683897,4.23895932023555));
#69674=CARTESIAN_POINT('Ctrl Pts',(4.18785084798745,-4.2608986517151,4.0819608268935));
#69675=CARTESIAN_POINT('Ctrl Pts',(-1.24365772802729,-5.8435149929827,3.92496233355144));
#69676=CARTESIAN_POINT('Ctrl Pts',(-5.55998778444767,-2.18629546534688,
3.76796384020939));
#69677=CARTESIAN_POINT('Ctrl Pts',(-4.89071868571119,3.43135874796699,3.61096534686732));
#69678=CARTESIAN_POINT('Ctrl Pts',(0.164021032340792,5.97213939901987,3.45396685352527));
#69679=CARTESIAN_POINT('Ctrl Pts',(5.07168429591276,3.15774768001703,3.29696836018321));
#69680=CARTESIAN_POINT('Ctrl Pts',(5.43160651478565,-2.48817267483047,3.13996986684115));
#69681=CARTESIAN_POINT('Ctrl Pts',(0.921047975843499,-5.90296718493849,
2.9829713734991));
#69682=CARTESIAN_POINT('Ctrl Pts',(-4.41540712917277,-4.02461577647203,
2.82597288015704));
#69683=CARTESIAN_POINT('Ctrl Pts',(-5.79260033662206,1.46257883627908,2.66897438681498));
#69684=CARTESIAN_POINT('Ctrl Pts',(-1.97561166336026,5.63828895889383,2.51197589347292));
#69685=CARTESIAN_POINT('Ctrl Pts',(3.6128915810316,4.75818989009414,2.35497740013087));
#69686=CARTESIAN_POINT('Ctrl Pts',(5.96174508817349,-0.388546134793637,
2.19797890678881));
#69687=CARTESIAN_POINT('Ctrl Pts',(2.96474106500057,-5.18686823314646,2.04098041344675));
#69688=CARTESIAN_POINT('Ctrl Pts',(-2.69071315072611,-5.33417912211988,
1.88398192010469));
#69689=CARTESIAN_POINT('Ctrl Pts',(-5.93344585957197,-0.698344012997689,
1.72698342676263));
#69690=CARTESIAN_POINT('Ctrl Pts',(-3.85566261618328,4.5636376221251,1.56998493342058));
#69691=CARTESIAN_POINT('Ctrl Pts',(1.67938795492248,5.73354207176578,1.41298644007852));
#69692=CARTESIAN_POINT('Ctrl Pts',(5.70869045070874,1.76202618095205,1.25598794673646));
#69693=CARTESIAN_POINT('Ctrl Pts',(4.61877209773216,-3.78910839602635,1.0989894533944));
#69694=CARTESIAN_POINT('Ctrl Pts',(-0.612224753988487,-5.94330155793046,
0.941990960052346));
#69695=CARTESIAN_POINT('Ctrl Pts',(-5.29528029823663,-2.76679183543498,
0.784992466710288));
#69696=CARTESIAN_POINT('Ctrl Pts',(-5.22810794124132,2.88801019068349,0.62799397336823));
#69697=CARTESIAN_POINT('Ctrl Pts',(-0.476761969141785,5.95830217192949,
0.470995480026171));
#69698=CARTESIAN_POINT('Ctrl Pts',(4.70955374493753,3.67573393888292,0.313996986684114));
#69699=CARTESIAN_POINT('Ctrl Pts',(5.49957691269067,-0.955274817987675,
0.183164908899066));
#69700=CARTESIAN_POINT('Ctrl Pts',(3.61105296193539,-3.84612671226304,0.0784992466710263));
#69701=CARTESIAN_POINT('Ctrl Pts',(2.11876087752236,-4.68487601374969,0.0261664155570096));
#69702=CARTESIAN_POINT('Ctrl Pts',(1.31303618635654,-4.90075024188321,0.));
#69703=CARTESIAN_POINT('Ctrl Pts',(1.31303618635654,-4.90075024188321,0.));
#69704=CARTESIAN_POINT('Ctrl Pts',(1.45239813196613,-4.85517621763986,-2.47434559251786E-16));
#69705=CARTESIAN_POINT('Ctrl Pts',(1.58927692318379,-4.80351009978137,-1.74819720228364E-15));
#69706=CARTESIAN_POINT('Ctrl Pts',(1.72341090925204,-4.74604460400692,-1.88737914186277E-15));
#69707=CARTESIAN_POINT('Ctrl Pts',(1.85925417986306,-4.68784681892573,-2.02833469262672E-15));
#69708=CARTESIAN_POINT('Ctrl Pts',(1.99228283138741,-4.62370052461763,2.98138735348004E-16));
#69709=CARTESIAN_POINT('Ctrl Pts',(2.12220346118141,-4.55386096654418,1.11022302462516E-16));
#69710=CARTESIAN_POINT('Ctrl Pts',(2.25247560296862,-4.48383245124121,-7.66003908251115E-17));
#69711=CARTESIAN_POINT('Ctrl Pts',(2.37962344910693,-4.40807936214696,-4.32517766211178E-16));
#69712=CARTESIAN_POINT('Ctrl Pts',(2.50332095055395,-4.32681677710386,-4.44089209850063E-16));
#69713=CARTESIAN_POINT('Ctrl Pts',(2.62609735089877,-4.24615930579203,-4.55574487888469E-16));
#69714=CARTESIAN_POINT('Ctrl Pts',(2.74547509807873,-4.16007358686041,1.08564249317406E-16));
#69715=CARTESIAN_POINT('Ctrl Pts',(2.86109774307792,-4.06873562676994,-5.55111512312578E-17));
#69716=CARTESIAN_POINT('Ctrl Pts',(2.90211866182286,-4.03633049506564,-1.13722271327984E-16));
#69717=CARTESIAN_POINT('Ctrl Pts',(2.94266654026491,-4.00326397860027,-2.92134559916121E-15));
#69718=CARTESIAN_POINT('Ctrl Pts',(2.98272412781597,-3.96954306736407,-2.99760216648792E-15));
#69719=CARTESIAN_POINT('Ctrl Pts',(2.99979215651063,-3.95517501587181,-3.03009412016909E-15));
#69720=CARTESIAN_POINT('Ctrl Pts',(3.01677225892353,-3.94068710954429,-2.12566972362838E-15));
#69721=CARTESIAN_POINT('Ctrl Pts',(3.03364729547102,-3.92609378878367,-2.1094237467878E-15));
#69722=CARTESIAN_POINT('Ctrl Pts',(3.14433957478624,-3.83036848867988,-2.00285780240447E-15));
#69723=CARTESIAN_POINT('Ctrl Pts',(3.25067225380611,-3.72997908311154,-3.12896148123733E-15));
#69724=CARTESIAN_POINT('Ctrl Pts',(3.35235973413124,-3.62516300488518,-3.10862446895044E-15));
#69725=CARTESIAN_POINT('Ctrl Pts',(3.36192986162372,-3.61529843523825,-3.10671048898182E-15));
#69726=CARTESIAN_POINT('Ctrl Pts',(3.37145882014037,-3.60539462864919,-2.66105468162811E-15));
#69727=CARTESIAN_POINT('Ctrl Pts',(3.38094635546186,-3.59545176562119,-2.692290834716E-15));
#69728=CARTESIAN_POINT('Ctrl Pts',(3.48180408426425,-3.48975365237926,-3.02597608841997E-15));
#69729=CARTESIAN_POINT('Ctrl Pts',(3.57798405787049,-3.37964444416285,-3.04382432431275E-15));
#69730=CARTESIAN_POINT('Ctrl Pts',(3.66918347167548,-3.26550314479251,-2.94209101525666E-15));
#69731=CARTESIAN_POINT('Ctrl Pts',(3.75971565071324,-3.15219692801907,-2.84110200923889E-15));
#69732=CARTESIAN_POINT('Ctrl Pts',(3.84534031026112,-3.03491668112307,-1.42999735083781E-15));
#69733=CARTESIAN_POINT('Ctrl Pts',(3.92571655230007,-2.91400844798661,-1.72084568816899E-15));
#69734=CARTESIAN_POINT('Ctrl Pts',(3.99657720672258,-2.80741430638731,-1.97726105417974E-15));
#69735=CARTESIAN_POINT('Ctrl Pts',(4.06335815473368,-2.69799970084542,-4.7182430533371E-15));
#69736=CARTESIAN_POINT('Ctrl Pts',(4.12579259176727,-2.58599222827228,-4.96824803519758E-15));
#69737=CARTESIAN_POINT('Ctrl Pts',(4.14218217787996,-2.55658928649489,-5.03387653084013E-15));
#69738=CARTESIAN_POINT('Ctrl Pts',(4.15827206325859,-2.52700763769101,-2.22246092678142E-15));
#69739=CARTESIAN_POINT('Ctrl Pts',(4.17405702945515,-2.49725134739943,-2.08166817117217E-15));
#69740=CARTESIAN_POINT('Ctrl Pts',(4.18546582852437,-2.47574458376403,-1.97990829160411E-15));
#69741=CARTESIAN_POINT('Ctrl Pts',(4.1967169159508,-2.45414332829404,-3.10559938199478E-15));
#69742=CARTESIAN_POINT('Ctrl Pts',(4.20779634099434,-2.4324729617879,-3.08086889333481E-15));
#69743=CARTESIAN_POINT('Ctrl Pts',(4.27314972651924,-2.30464757272886,-2.93499298792804E-15));
#69744=CARTESIAN_POINT('Ctrl Pts',(4.3326198595779,-2.17426195525281,-5.03888835755339E-15));
#69745=CARTESIAN_POINT('Ctrl Pts',(4.38592260758549,-2.04167340157391,-4.413136522885E-15));
#69746=CARTESIAN_POINT('Ctrl Pts',(4.43841100193019,-1.9111105215869,-3.79694485758248E-15));
#69747=CARTESIAN_POINT('Ctrl Pts',(4.48491932736646,-1.77841080748911,-3.47246432590996E-15));
#69748=CARTESIAN_POINT('Ctrl Pts',(4.52512906800885,-1.64389810614591,-3.30291349825984E-15));
#69749=CARTESIAN_POINT('Ctrl Pts',(4.53704337373435,-1.60404145892158,-3.25267491516128E-15));
#69750=CARTESIAN_POINT('Ctrl Pts',(4.54840435272953,-1.56402555907027,-1.86047514559207E-15));
#69751=CARTESIAN_POINT('Ctrl Pts',(4.55920284487768,-1.52385866802948,-1.74860126378462E-15));
#69752=CARTESIAN_POINT('Ctrl Pts',(4.59648625924208,-1.38517645000696,-1.33619040184573E-15));
#69753=CARTESIAN_POINT('Ctrl Pts',(4.62706837090021,-1.24469418107576,-3.1405520603229E-15));
#69754=CARTESIAN_POINT('Ctrl Pts',(4.6510479415724,-1.1028549274787,-3.44169137633799E-15));
#69755=CARTESIAN_POINT('Ctrl Pts',(4.66553556506662,-1.0171605782801,-3.62362928879583E-15));
#69756=CARTESIAN_POINT('Ctrl Pts',(4.67761212738266,-0.93097088404131,-3.48256637849421E-15));
#69757=CARTESIAN_POINT('Ctrl Pts',(4.68729033896278,-0.844384764732073,
-3.60822483003176E-15));
#69758=CARTESIAN_POINT('Ctrl Pts',(4.69282045363923,-0.794909594117687,
-3.68002586902689E-15));
#69759=CARTESIAN_POINT('Ctrl Pts',(4.6975673931995,-0.74530501799734,-2.90670583210387E-15));
#69760=CARTESIAN_POINT('Ctrl Pts',(4.70153256693874,-0.695589781678817,
-3.02535774210355E-15));
#69761=CARTESIAN_POINT('Ctrl Pts',(4.70300273002319,-0.67715691846114,-3.06935017962366E-15));
#69762=CARTESIAN_POINT('Ctrl Pts',(4.70436508297707,-0.658712562708346,
-1.39035176949888E-15));
#69763=CARTESIAN_POINT('Ctrl Pts',(4.70561925922056,-0.640267374588028,
-1.41553435639707E-15));
#69764=CARTESIAN_POINT('Ctrl Pts',(4.71515008316959,-0.500097409167311,
-1.60690363448191E-15));
#69765=CARTESIAN_POINT('Ctrl Pts',(4.71845154780466,-0.359714693128242,
-6.98970443009747E-16));
#69766=CARTESIAN_POINT('Ctrl Pts',(4.71567835888356,-0.219533504962576,
-9.0205620750794E-16));
#69767=CARTESIAN_POINT('Ctrl Pts',(4.71285964179518,-0.0770509255950372,
-1.1084760840775E-15));
#69768=CARTESIAN_POINT('Ctrl Pts',(4.70376507114378,0.065224279671225,-2.40577940367026E-15));
#69769=CARTESIAN_POINT('Ctrl Pts',(4.68850374693714,0.206855299208619,-2.26207941267376E-15));
#69770=CARTESIAN_POINT('Ctrl Pts',(4.67332604169022,0.347710302303635,-2.11916677430768E-15));
#69771=CARTESIAN_POINT('Ctrl Pts',(4.65204869880232,0.487928957857132,-3.70693630030531E-15));
#69772=CARTESIAN_POINT('Ctrl Pts',(4.62472984685344,0.627067645312151,-4.06619182768964E-15));
#69773=CARTESIAN_POINT('Ctrl Pts',(4.60512526025429,0.72691651350792,-4.32400120090221E-15));
#69774=CARTESIAN_POINT('Ctrl Pts',(4.58240838869996,0.826208961746935,-2.80327058352682E-15));
#69775=CARTESIAN_POINT('Ctrl Pts',(4.55658611607818,0.924773126569175,-2.94209101525666E-15));
#69776=CARTESIAN_POINT('Ctrl Pts',(4.54451163215688,0.970861688981747,-3.00700339130591E-15));
#69777=CARTESIAN_POINT('Ctrl Pts',(4.53175798542344,1.01679090044476,-4.8702446610021E-15));
#69778=CARTESIAN_POINT('Ctrl Pts',(4.51832500803005,1.062542528366,-4.8988590961585E-15));
#69779=CARTESIAN_POINT('Ctrl Pts',(4.51266846717592,1.08180824622589,-4.91090845176596E-15));
#69780=CARTESIAN_POINT('Ctrl Pts',(4.50689146090876,1.10104246936981,-1.58247074004002E-15));
#69781=CARTESIAN_POINT('Ctrl Pts',(4.50099394804091,1.12024381085806,-1.56819002228303E-15));
#69782=CARTESIAN_POINT('Ctrl Pts',(4.49471177106765,1.14069755603102,-1.55297784754686E-15));
#69783=CARTESIAN_POINT('Ctrl Pts',(4.48829554526876,1.1611051847425,-3.02768046308214E-15));
#69784=CARTESIAN_POINT('Ctrl Pts',(4.48174652480305,1.18146221251882,-3.05311331771918E-15));
#69785=CARTESIAN_POINT('Ctrl Pts',(4.4388367801027,1.31484320732769,-3.21975156617037E-15));
#69786=CARTESIAN_POINT('Ctrl Pts',(4.3902172033679,1.44609540153194,-2.42101694317024E-15));
#69787=CARTESIAN_POINT('Ctrl Pts',(4.33595560037894,1.57478564497199,-2.33146835171283E-15));
#69788=CARTESIAN_POINT('Ctrl Pts',(4.28905400984558,1.68602041819998,-2.25406607942409E-15));
#69789=CARTESIAN_POINT('Ctrl Pts',(4.23793630897375,1.79534112442678,-2.09120843630436E-15));
#69790=CARTESIAN_POINT('Ctrl Pts',(4.18261934387559,1.90245063170277,-1.54737334057131E-15));
#69791=CARTESIAN_POINT('Ctrl Pts',(4.15876651886949,1.94863654101668,-1.31287017598733E-15));
#69792=CARTESIAN_POINT('Ctrl Pts',(4.13413259613109,1.99441106904023,-3.34114378130206E-15));
#69793=CARTESIAN_POINT('Ctrl Pts',(4.1087175751394,2.03974918362091,-3.32373017997156E-15));
#69794=CARTESIAN_POINT('Ctrl Pts',(4.09757084929567,2.05963394128716,-3.31609278159812E-15));
#69795=CARTESIAN_POINT('Ctrl Pts',(4.08627386148571,2.07943474030452,-3.10826804513356E-15));
#69796=CARTESIAN_POINT('Ctrl Pts',(4.07482656400744,2.09914941832117,-3.21964677141295E-15));
#69797=CARTESIAN_POINT('Ctrl Pts',(4.06286705490573,2.11974623356295,-3.33600916115644E-15));
#69798=CARTESIAN_POINT('Ctrl Pts',(4.05074796307183,2.14024130439856,-5.56609850953026E-16));
#69799=CARTESIAN_POINT('Ctrl Pts',(4.03847105489573,2.16062996612303,-7.21644966006352E-16));
#69800=CARTESIAN_POINT('Ctrl Pts',(3.96920184151707,2.27566760746066,-1.65281203475204E-15));
#69801=CARTESIAN_POINT('Ctrl Pts',(3.89489673126452,2.38734604756407,-5.44084181235126E-15));
#69802=CARTESIAN_POINT('Ctrl Pts',(3.81559015152877,2.49525778868992,-3.92741394961149E-15));
#69803=CARTESIAN_POINT('Ctrl Pts',(3.73966418517796,2.5985695599563,-2.47849920176032E-15));
#69804=CARTESIAN_POINT('Ctrl Pts',(3.65915364949516,2.69842924853399,9.77632756533034E-16));
#69805=CARTESIAN_POINT('Ctrl Pts',(3.57405694815596,2.79444772885285,1.90646110009851E-15));
#69806=CARTESIAN_POINT('Ctrl Pts',(3.53072890723773,2.84333672899846,2.33391700333807E-15));
#69807=CARTESIAN_POINT('Ctrl Pts',(3.48621138925297,2.89122932971802,2.44271821993007E-16));
#69808=CARTESIAN_POINT('Ctrl Pts',(3.44055068766011,2.93810645203839,2.77555756156289E-16));
#69809=CARTESIAN_POINT('Ctrl Pts',(3.43378788736183,2.93584158413004,8.));
#69810=CARTESIAN_POINT('Ctrl Pts',(3.52723828091404,2.83914431545175,8.));
#69811=CARTESIAN_POINT('Ctrl Pts',(3.61594081851665,2.73846055769803,8.));
#69812=CARTESIAN_POINT('Ctrl Pts',(3.69984090589852,2.63418809372837,8.));
#69813=CARTESIAN_POINT('Ctrl Pts',(3.78516287227981,2.52814849421259,8.));
#69814=CARTESIAN_POINT('Ctrl Pts',(3.86551863442571,2.41839706286655,8.));
#69815=CARTESIAN_POINT('Ctrl Pts',(3.94081955158113,2.30530820215193,8.));
#69816=CARTESIAN_POINT('Ctrl Pts',(4.01714046916727,2.19068747846675,8.));
#69817=CARTESIAN_POINT('Ctrl Pts',(4.08826910733635,2.07263776324572,8.));
#69818=CARTESIAN_POINT('Ctrl Pts',(4.15407500660322,1.95151170764482,8.));
#69819=CARTESIAN_POINT('Ctrl Pts',(4.2198164513151,1.83050429073889,8.));
#69820=CARTESIAN_POINT('Ctrl Pts',(4.28024594506117,1.70642592249187,8.));
#69821=CARTESIAN_POINT('Ctrl Pts',(4.33518967485951,1.57960030623271,8.));
#69822=CARTESIAN_POINT('Ctrl Pts',(4.35307625782352,1.53831303076909,8.));
#69823=CARTESIAN_POINT('Ctrl Pts',(4.37038109771682,1.49673442540794,8.));
#69824=CARTESIAN_POINT('Ctrl Pts',(4.3870970941841,1.45487519313349,8.));
#69825=CARTESIAN_POINT('Ctrl Pts',(4.39376575085273,1.43817592851012,8.));
#69826=CARTESIAN_POINT('Ctrl Pts',(4.40033736934907,1.42144028204873,8.));
#69827=CARTESIAN_POINT('Ctrl Pts',(4.40681102745828,1.40467100393547,8.));
#69828=CARTESIAN_POINT('Ctrl Pts',(4.45934053196233,1.26859927210788,8.));
#69829=CARTESIAN_POINT('Ctrl Pts',(4.50544025366947,1.13027539792009,8.));
#69830=CARTESIAN_POINT('Ctrl Pts',(4.54499873531868,0.990127463611741,8.));
#69831=CARTESIAN_POINT('Ctrl Pts',(4.58299050839006,0.855530070216331,8.));
#69832=CARTESIAN_POINT('Ctrl Pts',(4.61494911931547,0.719249512352558,8.));
#69833=CARTESIAN_POINT('Ctrl Pts',(4.64085249468742,0.581767615475945,8.));
#69834=CARTESIAN_POINT('Ctrl Pts',(4.66691769963291,0.443426809811538,8.));
#69835=CARTESIAN_POINT('Ctrl Pts',(4.68685201899535,0.303868786404607,8.));
#69836=CARTESIAN_POINT('Ctrl Pts',(4.70058414747143,0.163565049614876,8.));
#69837=CARTESIAN_POINT('Ctrl Pts',(4.71271762019861,0.0395950789853681,
8.));
#69838=CARTESIAN_POINT('Ctrl Pts',(4.72000832561645,-0.0849577470138994,
8.));
#69839=CARTESIAN_POINT('Ctrl Pts',(4.7223733384523,-0.209772800136726,8.));
#69840=CARTESIAN_POINT('Ctrl Pts',(4.72292943816615,-0.239121315406544,
8.));
#69841=CARTESIAN_POINT('Ctrl Pts',(4.7232130590816,-0.268484329285888,8.));
#69842=CARTESIAN_POINT('Ctrl Pts',(4.72322285747563,-0.297857662780827,
8.));
#69843=CARTESIAN_POINT('Ctrl Pts',(4.72323033779459,-0.320281939952091,
8.));
#69844=CARTESIAN_POINT('Ctrl Pts',(4.72307812055779,-0.342714494826838,
8.));
#69845=CARTESIAN_POINT('Ctrl Pts',(4.72276611337907,-0.365130653249834,
8.));
#69846=CARTESIAN_POINT('Ctrl Pts',(4.72077139214363,-0.508441417465993,
8.));
#69847=CARTESIAN_POINT('Ctrl Pts',(4.71225120797944,-0.651280085007766,
8.));
#69848=CARTESIAN_POINT('Ctrl Pts',(4.69718547532262,-0.793154607131843,
8.));
#69849=CARTESIAN_POINT('Ctrl Pts',(4.68212772666397,-0.934953943670782,
8.));
#69850=CARTESIAN_POINT('Ctrl Pts',(4.66053153776914,-1.07579102267899,8.));
#69851=CARTESIAN_POINT('Ctrl Pts',(4.63232650453452,-1.21518583219434,8.));
#69852=CARTESIAN_POINT('Ctrl Pts',(4.62517817164043,-1.25051429622537,8.));
#69853=CARTESIAN_POINT('Ctrl Pts',(4.6176050749471,-1.28575013896589,8.));
#69854=CARTESIAN_POINT('Ctrl Pts',(4.60960553319191,-1.32088555816255,8.));
#69855=CARTESIAN_POINT('Ctrl Pts',(4.57835655312357,-1.45813667176012,8.));
#69856=CARTESIAN_POINT('Ctrl Pts',(4.54060431924761,-1.59385616146054,8.));
#69857=CARTESIAN_POINT('Ctrl Pts',(4.49667031501799,-1.72776662727194,8.));
#69858=CARTESIAN_POINT('Ctrl Pts',(4.46792000249182,-1.81539733178229,8.));
#69859=CARTESIAN_POINT('Ctrl Pts',(4.43652132007444,-1.90225320075805,8.));
#69860=CARTESIAN_POINT('Ctrl Pts',(4.4025528899726,-1.98825323145006,8.));
#69861=CARTESIAN_POINT('Ctrl Pts',(4.39064088821649,-2.01841160243036,8.));
#69862=CARTESIAN_POINT('Ctrl Pts',(4.37841279355623,-2.04846469658551,8.));
#69863=CARTESIAN_POINT('Ctrl Pts',(4.36587175340618,-2.07840891566329,8.));
#69864=CARTESIAN_POINT('Ctrl Pts',(4.35885849939885,-2.09515444968045,8.));
#69865=CARTESIAN_POINT('Ctrl Pts',(4.35174737519127,-2.11186593393486,8.));
#69866=CARTESIAN_POINT('Ctrl Pts',(4.34453891478344,-2.12854273059161,8.));
#69867=CARTESIAN_POINT('Ctrl Pts',(4.33664233992457,-2.14681148227446,8.));
#69868=CARTESIAN_POINT('Ctrl Pts',(4.32863248368416,-2.16503040522278,8.));
#69869=CARTESIAN_POINT('Ctrl Pts',(4.32051229345552,-2.18319454758947,8.));
#69870=CARTESIAN_POINT('Ctrl Pts',(4.26271734267779,-2.31247670532764,8.));
#69871=CARTESIAN_POINT('Ctrl Pts',(4.19930769062008,-2.43905306787665,8.));
#69872=CARTESIAN_POINT('Ctrl Pts',(4.1306563766664,-2.56266246904431,8.));
#69873=CARTESIAN_POINT('Ctrl Pts',(4.05932719227651,-2.69109348165625,8.));
#69874=CARTESIAN_POINT('Ctrl Pts',(3.98233931388035,-2.81632224208436,8.));
#69875=CARTESIAN_POINT('Ctrl Pts',(3.90005514682149,-2.93804448640157,8.));
#69876=CARTESIAN_POINT('Ctrl Pts',(3.81788412514087,-3.05959935575629,8.));
#69877=CARTESIAN_POINT('Ctrl Pts',(3.73043085662906,-3.17765799919859,8.));
#69878=CARTESIAN_POINT('Ctrl Pts',(3.63800695579095,-3.29189623321801,8.));
#69879=CARTESIAN_POINT('Ctrl Pts',(3.56857767496828,-3.37771254651463,8.));
#69880=CARTESIAN_POINT('Ctrl Pts',(3.49634236728105,-3.46137260211582,8.));
#69881=CARTESIAN_POINT('Ctrl Pts',(3.42141741611953,-3.54272769601374,8.));
#69882=CARTESIAN_POINT('Ctrl Pts',(3.38628453897598,-3.58087571579362,8.));
#69883=CARTESIAN_POINT('Ctrl Pts',(3.35056009922657,-3.61851677693959,8.));
#69884=CARTESIAN_POINT('Ctrl Pts',(3.3142552023334,-3.65563464117867,8.));
#69885=CARTESIAN_POINT('Ctrl Pts',(3.299200603776,-3.67102635395701,8.));
#69886=CARTESIAN_POINT('Ctrl Pts',(3.28404454782071,-3.68632972667595,8.));
#69887=CARTESIAN_POINT('Ctrl Pts',(3.26879310797022,-3.70153828550149,8.));
#69888=CARTESIAN_POINT('Ctrl Pts',(3.16313496534899,-3.80689935915782,8.));
#69889=CARTESIAN_POINT('Ctrl Pts',(3.05310906400962,-3.90750842604698,8.));
#69890=CARTESIAN_POINT('Ctrl Pts',(2.93905349297435,-4.00304219163214,8.));
#69891=CARTESIAN_POINT('Ctrl Pts',(2.83343523748027,-4.09150880111292,8.));
#69892=CARTESIAN_POINT('Ctrl Pts',(2.72436063892977,-4.17562341526862,8.));
#69893=CARTESIAN_POINT('Ctrl Pts',(2.61206707761722,-4.25510461849443,8.));
#69894=CARTESIAN_POINT('Ctrl Pts',(2.56057116079448,-4.29155334611912,8.));
#69895=CARTESIAN_POINT('Ctrl Pts',(2.50839792228814,-4.3270273021059,8.));
#69896=CARTESIAN_POINT('Ctrl Pts',(2.45556847535629,-4.3614972584752,8.));
#69897=CARTESIAN_POINT('Ctrl Pts',(2.42827791858812,-4.37930369703788,8.));
#69898=CARTESIAN_POINT('Ctrl Pts',(2.40081223344856,-4.39684219182932,8.));
#69899=CARTESIAN_POINT('Ctrl Pts',(2.37317422709578,-4.41410855841438,8.));
#69900=CARTESIAN_POINT('Ctrl Pts',(2.35241127848289,-4.42707985155184,8.));
#69901=CARTESIAN_POINT('Ctrl Pts',(2.33155925321721,-4.43989244410762,8.));
#69902=CARTESIAN_POINT('Ctrl Pts',(2.31062069154639,-4.45254421740167,8.));
#69903=CARTESIAN_POINT('Ctrl Pts',(2.18359867140573,-4.52929513408044,8.));
#69904=CARTESIAN_POINT('Ctrl Pts',(2.05338150515115,-4.60013897577206,8.00000000000001));
#69905=CARTESIAN_POINT('Ctrl Pts',(1.9202708514578,-4.66473499429566,8.00000000000001));
#69906=CARTESIAN_POINT('Ctrl Pts',(1.79118849882964,-4.72737615644222,8.00000000000001));
#69907=CARTESIAN_POINT('Ctrl Pts',(1.65938453798209,-4.78414231274042,8.00000000000001));
#69908=CARTESIAN_POINT('Ctrl Pts',(1.52510693593821,-4.83468454964306,8.00000000000001));
#69909=CARTESIAN_POINT('Ctrl Pts',(1.45664940136588,-4.86045204085127,8.00000000000001));
#69910=CARTESIAN_POINT('Ctrl Pts',(1.38754853402863,-4.88460115986285,8.00000000000001));
#69911=CARTESIAN_POINT('Ctrl Pts',(1.31785785677859,-4.9071457994741,8.00000000000001));
#69912=CARTESIAN_POINT('Ctrl Pts',(-4.51611343680291,-0.0038242599945422,
6.38741669750802));
#69913=CARTESIAN_POINT('Ctrl Pts',(-4.51950916701914,-0.407146869176555,
6.40161615386516));
#69914=CARTESIAN_POINT('Ctrl Pts',(-4.46982237313174,-0.809647705501708,
6.41581561022229));
#69915=CARTESIAN_POINT('Ctrl Pts',(-4.36369015740015,-1.19666942701374,
6.43001506657943));
#69916=CARTESIAN_POINT('Ctrl Pts',(-3.97253438481685,-2.62305800696593,
6.48234789769345));
#69917=CARTESIAN_POINT('Ctrl Pts',(-2.81466398536927,-3.83918925602438,
6.53468072880746));
#69918=CARTESIAN_POINT('Ctrl Pts',(-1.40915345298166,-4.2997974804633,6.58701355992148));
#69919=CARTESIAN_POINT('Ctrl Pts',(-0.0036429205940397,-4.76040570490222,
6.6393463910355));
#69920=CARTESIAN_POINT('Ctrl Pts',(1.64950774473362,-4.4654909047216,6.69167922214952));
#69921=CARTESIAN_POINT('Ctrl Pts',(2.8090142019341,-3.54731124324962,6.74401205326355));
#69922=CARTESIAN_POINT('Ctrl Pts',(3.96852065913458,-2.62913158177766,6.79634488437757));
#69923=CARTESIAN_POINT('Ctrl Pts',(4.63438290820789,-1.08768705901433,6.84867771549158));
#69924=CARTESIAN_POINT('Ctrl Pts',(4.50825697351113,0.385987175391315,6.9010105466056));
#69925=CARTESIAN_POINT('Ctrl Pts',(4.38213103881437,1.85966140979697,6.95334337771962));
#69926=CARTESIAN_POINT('Ctrl Pts',(3.46401692034753,3.26556535584495,7.00567620883364));
#69927=CARTESIAN_POINT('Ctrl Pts',(2.16517738469227,3.97324114256653,7.05800903994766));
#69928=CARTESIAN_POINT('Ctrl Pts',(0.866337849037014,4.6809169292881,7.11034187106168));
#69929=CARTESIAN_POINT('Ctrl Pts',(-0.81322710380666,4.69036455668328,7.1626747021757));
#69930=CARTESIAN_POINT('Ctrl Pts',(-2.11977974996502,3.9975905624503,7.21500753328971));
#69931=CARTESIAN_POINT('Ctrl Pts',(-3.42633239612339,3.30481656821732,7.26734036440373));
#69932=CARTESIAN_POINT('Ctrl Pts',(-4.35987273559643,1.90982095235617,7.31967319551775));
#69933=CARTESIAN_POINT('Ctrl Pts',(-4.50322023061811,0.437577444110917,
7.37200602663177));
#69934=CARTESIAN_POINT('Ctrl Pts',(-4.51729094569115,0.293064846108908,
7.37714291692385));
#69935=CARTESIAN_POINT('Ctrl Pts',(-4.52374814565307,0.14780796397411,7.38227980721594));
#69936=CARTESIAN_POINT('Ctrl Pts',(-4.52286359173795,0.00246468782935438,
7.38741669750802));
#69937=CARTESIAN_POINT('Ctrl Pts',(-1.31303618635644,-4.90075024188323,
8.));
#69938=CARTESIAN_POINT('Ctrl Pts',(-2.11876087752226,-4.68487601374973,
7.97383358444299));
#69939=CARTESIAN_POINT('Ctrl Pts',(-3.61103600209076,-3.84612122823184,
7.92150075332897));
#69940=CARTESIAN_POINT('Ctrl Pts',(-5.49959712288033,-0.955281493922513,
7.81683509110094));
#69941=CARTESIAN_POINT('Ctrl Pts',(-4.70954440514987,3.67573693777646,7.68600301331588));
#69942=CARTESIAN_POINT('Ctrl Pts',(0.476758320675261,5.95830042580594,7.52900451997384));
#69943=CARTESIAN_POINT('Ctrl Pts',(5.22810884028568,2.88800998678043,7.37200602663177));
#69944=CARTESIAN_POINT('Ctrl Pts',(5.29527916712856,-2.76679132542031,7.21500753328971));
#69945=CARTESIAN_POINT('Ctrl Pts',(0.612224870220684,-5.9433011663707,7.05800903994766));
#69946=CARTESIAN_POINT('Ctrl Pts',(-4.61877163601819,-3.7891077783966,6.90101054660559));
#69947=CARTESIAN_POINT('Ctrl Pts',(-5.70868984087812,1.76202584286959,6.74401205326355));
#69948=CARTESIAN_POINT('Ctrl Pts',(-1.67938775292856,5.73354154736347,6.58701355992148));
#69949=CARTESIAN_POINT('Ctrl Pts',(3.85566217988192,4.56363706615652,6.43001506657943));
#69950=CARTESIAN_POINT('Ctrl Pts',(5.93344523009267,-0.69834389981148,6.27301657323736));
#69951=CARTESIAN_POINT('Ctrl Pts',(2.69071284975304,-5.33417856632519,6.11601807989532));
#69952=CARTESIAN_POINT('Ctrl Pts',(-2.96474073765194,-5.18686765769478,
5.95901958655325));
#69953=CARTESIAN_POINT('Ctrl Pts',(-5.96174444561926,-0.38854610033802,
5.8020210932112));
#69954=CARTESIAN_POINT('Ctrl Pts',(-3.61289118716291,4.75818937870979,5.64502259986913));
#69955=CARTESIAN_POINT('Ctrl Pts',(1.97561144788205,5.63828834519714,5.48802410652708));
#69956=CARTESIAN_POINT('Ctrl Pts',(5.79259970947732,1.46257867915377,5.33102561318502));
#69957=CARTESIAN_POINT('Ctrl Pts',(4.41540665009831,-4.0246153410012,5.17402711984296));
#69958=CARTESIAN_POINT('Ctrl Pts',(-0.92104787574744,-5.90296654461282,
5.01702862650091));
#69959=CARTESIAN_POINT('Ctrl Pts',(-5.43160592614493,-2.48817240536104,
4.86003013315885));
#69960=CARTESIAN_POINT('Ctrl Pts',(-5.07168374606222,3.15774733785514,4.70303163981679));
#69961=CARTESIAN_POINT('Ctrl Pts',(-0.164021014606317,5.97213875156532,
4.54603314647473));
#69962=CARTESIAN_POINT('Ctrl Pts',(4.89071815558305,3.43135837605058,4.38903465313268));
#69963=CARTESIAN_POINT('Ctrl Pts',(5.55998718173337,-2.18629522837624,4.23203615979062));
#69964=CARTESIAN_POINT('Ctrl Pts',(1.24365759322077,-5.84351435953346,4.07503766644856));
#69965=CARTESIAN_POINT('Ctrl Pts',(-4.1878503940255,-4.26089818984331,3.91803917310651));
#69966=CARTESIAN_POINT('Ctrl Pts',(-5.86414447963045,1.14243329300625,3.76104067976444));
#69967=CARTESIAN_POINT('Ctrl Pts',(-2.2821043825461,5.52135344516299,3.60404218642239));
#69968=CARTESIAN_POINT('Ctrl Pts',(3.34628151701835,4.94931755856517,3.44704369308033));
#69969=CARTESIAN_POINT('Ctrl Pts',(5.9740820006751,-0.0607341045204584,
3.29004519973827));
#69970=CARTESIAN_POINT('Ctrl Pts',(3.24496813195078,-5.01632594473331,3.13304670639622));
#69971=CARTESIAN_POINT('Ctrl Pts',(-2.39388416789017,-5.47381611497205,
2.97604821305415));
#69972=CARTESIAN_POINT('Ctrl Pts',(-5.88615866062065,-1.02297657731424,
2.8190497197121));
#69973=CARTESIAN_POINT('Ctrl Pts',(-4.10035884408111,4.34515829009749,2.66205122637004));
#69974=CARTESIAN_POINT('Ctrl Pts',(1.36220151697138,5.81702256793933,2.50505273302799));
#69975=CARTESIAN_POINT('Ctrl Pts',(5.60328669734595,2.07280630409542,2.34805423968593));
#69976=CARTESIAN_POINT('Ctrl Pts',(4.81994564291905,-3.53007932713903,2.19105574634387));
#69977=CARTESIAN_POINT('Ctrl Pts',(-0.285401937658034,-5.96757024490932,
2.03405725300181));
#69978=CARTESIAN_POINT('Ctrl Pts',(-5.13483640041478,-3.05398429071519,
1.87705875965975));
#69979=CARTESIAN_POINT('Ctrl Pts',(-5.37989282152843,2.59808332599247,1.7200602663177));
#69980=CARTESIAN_POINT('Ctrl Pts',(-0.800856996403053,5.92047503909791,
1.56306177297564));
#69981=CARTESIAN_POINT('Ctrl Pts',(4.49633411524324,3.93401017093414,1.40606327963358));
#69982=CARTESIAN_POINT('Ctrl Pts',(5.76163326143087,-1.58003046734643,1.24906478629152));
#69983=CARTESIAN_POINT('Ctrl Pts',(1.86064021890344,-5.67731097226746,1.09206629294947));
#69984=CARTESIAN_POINT('Ctrl Pts',(-3.70900698411085,-4.68371027734449,
0.935067799607409));
#69985=CARTESIAN_POINT('Ctrl Pts',(-5.9523702132809,0.509586132109229,0.77806930626535));
#69986=CARTESIAN_POINT('Ctrl Pts',(-2.85914249825567,5.24623219278067,0.621070812923292));
#69987=CARTESIAN_POINT('Ctrl Pts',(2.79949684465664,5.27806149196883,0.464072319581235));
#69988=CARTESIAN_POINT('Ctrl Pts',(5.94469888877439,0.578168532022547,0.307073826239177));
#69989=CARTESIAN_POINT('Ctrl Pts',(3.76540065952631,-4.64224087416102,0.150075332897119));
#69990=CARTESIAN_POINT('Ctrl Pts',(-1.80215437063507,-5.69588361575389,
-0.00692316044493745));
#69991=CARTESIAN_POINT('Ctrl Pts',(-5.07460576691081,-2.32518978947096,
-0.137755238229986));
#69992=CARTESIAN_POINT('Ctrl Pts',(-5.15385204348173,1.12695990370127,-0.242420900458024));
#69993=CARTESIAN_POINT('Ctrl Pts',(-4.39833476927544,2.66305504594052,-0.294753731572044));
#69994=CARTESIAN_POINT('Ctrl Pts',(-3.85627053850243,3.2970584607917,-0.320920147129053));
#69995=CARTESIAN_POINT('Ctrl Pts',(-1.26508527942735,-4.72177922709092,
8.10697338237635));
#69996=CARTESIAN_POINT('Ctrl Pts',(-2.04138562564518,-4.51378853265526,
8.08080696681934));
#69997=CARTESIAN_POINT('Ctrl Pts',(-3.47916419760203,-3.70566432158352,
8.02847413570533));
#69998=CARTESIAN_POINT('Ctrl Pts',(-5.29875675570167,-0.920395468326166,
7.92380847347728));
#69999=CARTESIAN_POINT('Ctrl Pts',(-4.53755605646894,3.54150231299569,7.79297639569223));
#70000=CARTESIAN_POINT('Ctrl Pts',(0.459347533295664,5.74070862434451,7.63597790235019));
#70001=CARTESIAN_POINT('Ctrl Pts',(5.03718298232336,2.78254244557681,7.47897940900812));
#70002=CARTESIAN_POINT('Ctrl Pts',(5.10190030891819,-2.66575058129155,7.32198091566607));
#70003=CARTESIAN_POINT('Ctrl Pts',(0.589866965635366,-5.72625712444602,
7.16498242232401));
#70004=CARTESIAN_POINT('Ctrl Pts',(-4.45009822766378,-3.650732951934,7.00798392898195));
#70005=CARTESIAN_POINT('Ctrl Pts',(-5.50021359468528,1.69767823533522,6.8509854356399));
#70006=CARTESIAN_POINT('Ctrl Pts',(-1.61805801451367,5.52415773908126,6.69398694229783));
#70007=CARTESIAN_POINT('Ctrl Pts',(3.71485684621434,4.39697712297199,6.53698844895578));
#70008=CARTESIAN_POINT('Ctrl Pts',(5.71676111814409,-0.672841005304612,
6.37998995561372));
#70009=CARTESIAN_POINT('Ctrl Pts',(2.5924504234985,-5.13937913685421,6.22299146227166));
#70010=CARTESIAN_POINT('Ctrl Pts',(-2.85647105806718,-4.99744789082776,
6.0659929689296));
#70011=CARTESIAN_POINT('Ctrl Pts',(-5.74402687163513,-0.374356744333544,
5.90899447558755));
#70012=CARTESIAN_POINT('Ctrl Pts',(-3.48095163297493,4.58442455911056,5.75199598224549));
#70013=CARTESIAN_POINT('Ctrl Pts',(1.90346388511891,5.43238309864782,5.59499748890343));
#70014=CARTESIAN_POINT('Ctrl Pts',(5.58105914994609,1.40916661416325,5.43799899556138));
#70015=CARTESIAN_POINT('Ctrl Pts',(4.25415994910644,-3.8776399890292,5.28100050221931));
#70016=CARTESIAN_POINT('Ctrl Pts',(-0.887412031262641,-5.68739548699278,
5.12400200887726));
#70017=CARTESIAN_POINT('Ctrl Pts',(-5.23324853664848,-2.39730657495003,
4.9670035155352));
#70018=CARTESIAN_POINT('Ctrl Pts',(-4.88647039260848,3.04242922988797,4.81000502219315));
#70019=CARTESIAN_POINT('Ctrl Pts',(-0.15803111388041,5.75404158682643,4.65300652885108));
#70020=CARTESIAN_POINT('Ctrl Pts',(4.71211350360807,3.30604823773145,4.49600803550903));
#70021=CARTESIAN_POINT('Ctrl Pts',(5.35694142362824,-2.10645368241985,4.33900954216697));
#70022=CARTESIAN_POINT('Ctrl Pts',(1.19824033044931,-5.63011444252866,4.18201104882491));
#70023=CARTESIAN_POINT('Ctrl Pts',(-4.03491384394147,-4.10529399960203,
4.02501255548286));
#70024=CARTESIAN_POINT('Ctrl Pts',(-5.6499911690947,1.10071265112688,3.86801406214079));
#70025=CARTESIAN_POINT('Ctrl Pts',(-2.19876397198699,5.31971855655701,3.71101556879874));
#70026=CARTESIAN_POINT('Ctrl Pts',(3.22407830948427,4.76857290881427,3.55401707545668));
#70027=CARTESIAN_POINT('Ctrl Pts',(5.75591387021709,-0.0585161493539971,
3.39701858211462));
#70028=CARTESIAN_POINT('Ctrl Pts',(3.12646479860794,-4.83313420866293,3.24002008877257));
#70029=CARTESIAN_POINT('Ctrl Pts',(-2.30646165956461,-5.27391724713939,
3.08302159543051));
#70030=CARTESIAN_POINT('Ctrl Pts',(-5.67120141188825,-0.985618387830106,
2.92602310208845));
#70031=CARTESIAN_POINT('Ctrl Pts',(-3.95061740713414,4.18647699637109,2.76902460874639));
#70032=CARTESIAN_POINT('Ctrl Pts',(1.31245513614984,5.60459010746491,2.61202611540434));
#70033=CARTESIAN_POINT('Ctrl Pts',(5.39865967966489,1.99710927213052,2.45502762206228));
#70034=CARTESIAN_POINT('Ctrl Pts',(4.64392553979592,-3.4011639879985,2.29802912872022));
#70035=CARTESIAN_POINT('Ctrl Pts',(-0.274979314205441,-5.74963991794669,
2.14103063537816));
#70036=CARTESIAN_POINT('Ctrl Pts',(-4.94731676851826,-2.94245551640673,
1.9840321420361));
#70037=CARTESIAN_POINT('Ctrl Pts',(-5.18342394835182,2.50320364708249,1.82703364869405));
#70038=CARTESIAN_POINT('Ctrl Pts',(-0.771610415313318,5.70426458692177,
1.67003515535199));
#70039=CARTESIAN_POINT('Ctrl Pts',(4.33213201561917,3.79034363872074,1.51303666200993));
#70040=CARTESIAN_POINT('Ctrl Pts',(5.55122356888078,-1.52232916811941,1.35603816866787));
#70041=CARTESIAN_POINT('Ctrl Pts',(1.79269130257332,-5.46998065428583,1.19903967532582));
#70042=CARTESIAN_POINT('Ctrl Pts',(-3.57355736700018,-4.5126653679007,1.04204118198376));
#70043=CARTESIAN_POINT('Ctrl Pts',(-5.73499497787591,0.490976502422684,
0.885042688641701));
#70044=CARTESIAN_POINT('Ctrl Pts',(-2.75472917190912,5.05464448619777,0.728044195299644));
#70045=CARTESIAN_POINT('Ctrl Pts',(2.6972617242226,5.08531140785296,0.571045701957586));
#70046=CARTESIAN_POINT('Ctrl Pts',(5.72760380327789,0.557054334442611,0.414047208615528));
#70047=CARTESIAN_POINT('Ctrl Pts',(3.62789159583729,-4.47271039022441,0.25704871527347));
#70048=CARTESIAN_POINT('Ctrl Pts',(-1.7363413051643,-5.48787504144657,0.100050221931414));
#70049=CARTESIAN_POINT('Ctrl Pts',(-4.88928570386961,-2.24027593839366,
-0.0307818558536355));
#70050=CARTESIAN_POINT('Ctrl Pts',(-4.96563797731115,1.08580433615736,-0.135447518081672));
#70051=CARTESIAN_POINT('Ctrl Pts',(-4.2377115180993,2.56580265793949,-0.187780349195693));
#70052=CARTESIAN_POINT('Ctrl Pts',(-3.71544298812226,3.17665283523778,-0.213946764752702));
#70053=CARTESIAN_POINT('Ctrl Pts',(-1.21713437249827,-4.54280821229861,
8.21394676475271));
#70054=CARTESIAN_POINT('Ctrl Pts',(-1.96401037376809,-4.34270105156078,
8.1877803491957));
#70055=CARTESIAN_POINT('Ctrl Pts',(-3.34729239311329,-3.56520741493521,
8.13544751808168));
#70056=CARTESIAN_POINT('Ctrl Pts',(-5.097916388523,-0.88550944272982,8.03078185585364));
#70057=CARTESIAN_POINT('Ctrl Pts',(-4.36556770778803,3.40726768821492,7.89994977806859));
#70058=CARTESIAN_POINT('Ctrl Pts',(0.441936745916073,5.52311682288307,7.74295128472654));
#70059=CARTESIAN_POINT('Ctrl Pts',(4.84625712436104,2.6770749043732,7.58595279138447));
#70060=CARTESIAN_POINT('Ctrl Pts',(4.90852145070782,-2.56470983716281,7.42895429804242));
#70061=CARTESIAN_POINT('Ctrl Pts',(0.567509061050049,-5.50921308252134,
7.27195580470035));
#70062=CARTESIAN_POINT('Ctrl Pts',(-4.28142481930937,-3.51235812547142,
7.11495731135831));
#70063=CARTESIAN_POINT('Ctrl Pts',(-5.29173734849243,1.63333062780086,6.95795881801624));
#70064=CARTESIAN_POINT('Ctrl Pts',(-1.55672827609878,5.31477393079903,6.80096032467419));
#70065=CARTESIAN_POINT('Ctrl Pts',(3.57405151254677,4.23031717978746,6.64396183133213));
#70066=CARTESIAN_POINT('Ctrl Pts',(5.50007700619551,-0.647338110797742,
6.48696333799007));
#70067=CARTESIAN_POINT('Ctrl Pts',(2.49418799724395,-4.94457970738323,6.32996484464802));
#70068=CARTESIAN_POINT('Ctrl Pts',(-2.74820137848241,-4.80802812396074,
6.17296635130595));
#70069=CARTESIAN_POINT('Ctrl Pts',(-5.52630929765102,-0.360167388329068,
6.0159678579639));
#70070=CARTESIAN_POINT('Ctrl Pts',(-3.34901207878694,4.41065973951134,5.85896936462184));
#70071=CARTESIAN_POINT('Ctrl Pts',(1.83131632235576,5.22647785209851,5.70197087127978));
#70072=CARTESIAN_POINT('Ctrl Pts',(5.36951859041486,1.35575454917273,5.54497237793772));
#70073=CARTESIAN_POINT('Ctrl Pts',(4.09291324811456,-3.73066463705719,5.38797388459567));
#70074=CARTESIAN_POINT('Ctrl Pts',(-0.853776186777843,-5.47182442937275,
5.23097539125361));
#70075=CARTESIAN_POINT('Ctrl Pts',(-5.03489114715202,-2.30644074453902,
5.07397689791155));
#70076=CARTESIAN_POINT('Ctrl Pts',(-4.70125703915474,2.92711112192079,4.91697840456949));
#70077=CARTESIAN_POINT('Ctrl Pts',(-0.1520412131545,5.53594442208755,4.75997991122743));
#70078=CARTESIAN_POINT('Ctrl Pts',(4.53350885163308,3.18073809941233,4.60298141788538));
#70079=CARTESIAN_POINT('Ctrl Pts',(5.15389566552312,-2.02661213646347,4.44598292454332));
#70080=CARTESIAN_POINT('Ctrl Pts',(1.15282306767785,-5.41671452552386,4.28898443120126));
#70081=CARTESIAN_POINT('Ctrl Pts',(-3.88197729385743,-3.94968980936076,
4.13198593785921));
#70082=CARTESIAN_POINT('Ctrl Pts',(-5.43583785855895,1.05899200924751,3.97498744451714));
#70083=CARTESIAN_POINT('Ctrl Pts',(-2.11542356142786,5.11808366795104,3.81798895117509));
#70084=CARTESIAN_POINT('Ctrl Pts',(3.1018751019502,4.58782825906337,3.66099045783304));
#70085=CARTESIAN_POINT('Ctrl Pts',(5.53774573975908,-0.0562981941875292,
3.50399196449097));
#70086=CARTESIAN_POINT('Ctrl Pts',(3.00796146526509,-4.64994247259256,3.34699347114892));
#70087=CARTESIAN_POINT('Ctrl Pts',(-2.21903915123905,-5.07401837930674,
3.18999497780685));
#70088=CARTESIAN_POINT('Ctrl Pts',(-5.45624416315586,-0.948260198345973,
3.03299648446481));
#70089=CARTESIAN_POINT('Ctrl Pts',(-3.80087597018717,4.0277957026447,2.87599799112274));
#70090=CARTESIAN_POINT('Ctrl Pts',(1.26270875532829,5.39215764699048,2.71899949778069));
#70091=CARTESIAN_POINT('Ctrl Pts',(5.19403266198385,1.92141224016561,2.56200100443863));
#70092=CARTESIAN_POINT('Ctrl Pts',(4.46790543667278,-3.27224864885797,2.40500251109657));
#70093=CARTESIAN_POINT('Ctrl Pts',(-0.264556690752847,-5.53170959098406,
2.24800401775451));
#70094=CARTESIAN_POINT('Ctrl Pts',(-4.75979713662174,-2.83092674209829,
2.09100552441246));
#70095=CARTESIAN_POINT('Ctrl Pts',(-4.9869550751752,2.40832396817252,1.9340070310704));
#70096=CARTESIAN_POINT('Ctrl Pts',(-0.742363834223583,5.48805413474563,
1.77700853772834));
#70097=CARTESIAN_POINT('Ctrl Pts',(4.16792991599511,3.64667710650734,1.62001004438628));
#70098=CARTESIAN_POINT('Ctrl Pts',(5.3408138763307,-1.4646278688924,1.46301155104423));
#70099=CARTESIAN_POINT('Ctrl Pts',(1.7247423862432,-5.26265033630419,1.30601305770217));
#70100=CARTESIAN_POINT('Ctrl Pts',(-3.43810774988952,-4.34162045845692,
1.14901456436011));
#70101=CARTESIAN_POINT('Ctrl Pts',(-5.51761974247093,0.472366872736146,
0.992016071018053));
#70102=CARTESIAN_POINT('Ctrl Pts',(-2.65031584556259,4.86305677961485,0.835017577675994));
#70103=CARTESIAN_POINT('Ctrl Pts',(2.59502660378856,4.89256132373709,0.678019084333937));
#70104=CARTESIAN_POINT('Ctrl Pts',(5.51050871778138,0.535940136862668,0.521020590991879));
#70105=CARTESIAN_POINT('Ctrl Pts',(3.49038253214829,-4.30317990628779,0.364022097649821));
#70106=CARTESIAN_POINT('Ctrl Pts',(-1.67052823969354,-5.27986646713926,
0.207023604307765));
#70107=CARTESIAN_POINT('Ctrl Pts',(-4.70396564082841,-2.15536208731635,
0.0761915265227156));
#70108=CARTESIAN_POINT('Ctrl Pts',(-4.77742391114056,1.04464876861345,-0.0284741357053212));
#70109=CARTESIAN_POINT('Ctrl Pts',(-4.07708826692317,2.46855026993846,-0.0808069668193416));
#70110=CARTESIAN_POINT('Ctrl Pts',(-3.57461543774208,3.05624720968387,-0.106973382376351));
#70111=CARTESIAN_POINT('Ctrl Pts',(-1.16918346556918,-4.3638371975063,8.32092014712906));
#70112=CARTESIAN_POINT('Ctrl Pts',(-1.886635121891,-4.17161357046631,8.29475373157205));
#70113=CARTESIAN_POINT('Ctrl Pts',(-3.21542058862456,-3.4247505082869,8.24242090045803));
#70114=CARTESIAN_POINT('Ctrl Pts',(-4.89707602134433,-0.850623417133479,
8.13775523822999));
#70115=CARTESIAN_POINT('Ctrl Pts',(-4.19357935910711,3.27303306343417,8.00692316044493));
#70116=CARTESIAN_POINT('Ctrl Pts',(0.424525958536476,5.30552502142163,7.84992466710289));
#70117=CARTESIAN_POINT('Ctrl Pts',(4.65533126639873,2.5716073631696,7.69292617376082));
#70118=CARTESIAN_POINT('Ctrl Pts',(4.71514259249745,-2.46366909303406,7.53592768041877));
#70119=CARTESIAN_POINT('Ctrl Pts',(0.545151156464739,-5.29216904059666,
7.3789291870767));
#70120=CARTESIAN_POINT('Ctrl Pts',(-4.11275141095498,-3.37398329900883,
7.22193069373466));
#70121=CARTESIAN_POINT('Ctrl Pts',(-5.08326110229957,1.56898302026649,7.06493220039259));
#70122=CARTESIAN_POINT('Ctrl Pts',(-1.4953985376839,5.10539012251682,6.90793370705054));
#70123=CARTESIAN_POINT('Ctrl Pts',(3.4332461788792,4.06365723660293,6.75093521370847));
#70124=CARTESIAN_POINT('Ctrl Pts',(5.28339289424692,-0.621835216290863,
6.59393672036643));
#70125=CARTESIAN_POINT('Ctrl Pts',(2.3959255709894,-4.74978027791225,6.43693822702436));
#70126=CARTESIAN_POINT('Ctrl Pts',(-2.63993169889764,-4.61860835709371,
6.27993973368231));
#70127=CARTESIAN_POINT('Ctrl Pts',(-5.3085917236669,-0.345978032324596,
6.12294124034025));
#70128=CARTESIAN_POINT('Ctrl Pts',(-3.21707252459896,4.23689491991211,5.96594274699819));
#70129=CARTESIAN_POINT('Ctrl Pts',(1.75916875959262,5.0205726055492,5.80894425365613));
#70130=CARTESIAN_POINT('Ctrl Pts',(5.15797803088363,1.30234248418222,5.65194576031408));
#70131=CARTESIAN_POINT('Ctrl Pts',(3.93166654712268,-3.58368928508518,5.49494726697202));
#70132=CARTESIAN_POINT('Ctrl Pts',(-0.820140342293046,-5.25625337175271,
5.33794877362996));
#70133=CARTESIAN_POINT('Ctrl Pts',(-4.83653375765556,-2.215574914128,5.1809502802879));
#70134=CARTESIAN_POINT('Ctrl Pts',(-4.516043685701,2.81179301395361,5.02395178694585));
#70135=CARTESIAN_POINT('Ctrl Pts',(-0.14605131242859,5.31784725734868,4.86695329360378));
#70136=CARTESIAN_POINT('Ctrl Pts',(4.3549041996581,3.0554279610932,4.70995480026174));
#70137=CARTESIAN_POINT('Ctrl Pts',(4.95084990741799,-1.94677059050708,4.55295630691967));
#70138=CARTESIAN_POINT('Ctrl Pts',(1.1074058049064,-5.20331460851906,4.39595781357761));
#70139=CARTESIAN_POINT('Ctrl Pts',(-3.7290407437734,-3.79408561911948,4.23895932023556));
#70140=CARTESIAN_POINT('Ctrl Pts',(-5.22168454802319,1.01727136736814,4.08196082689349));
#70141=CARTESIAN_POINT('Ctrl Pts',(-2.03208315086874,4.91644877934506,3.92496233355144));
#70142=CARTESIAN_POINT('Ctrl Pts',(2.97967189441612,4.40708360931248,3.76796384020938));
#70143=CARTESIAN_POINT('Ctrl Pts',(5.31957760930108,-0.0540802390210696,
3.61096534686732));
#70144=CARTESIAN_POINT('Ctrl Pts',(2.88945813192224,-4.46675073652217,3.45396685352527));
#70145=CARTESIAN_POINT('Ctrl Pts',(-2.13161664291348,-4.87411951147409,
3.29696836018321));
#70146=CARTESIAN_POINT('Ctrl Pts',(-5.24128691442347,-0.910902008861835,
3.13996986684115));
#70147=CARTESIAN_POINT('Ctrl Pts',(-3.6511345332402,3.86911440891831,2.9829713734991));
#70148=CARTESIAN_POINT('Ctrl Pts',(1.21296237450675,5.17972518651607,2.82597288015703));
#70149=CARTESIAN_POINT('Ctrl Pts',(4.98940564430279,1.8457152082007,2.66897438681498));
#70150=CARTESIAN_POINT('Ctrl Pts',(4.29188533354966,-3.14333330971743,2.51197589347292));
#70151=CARTESIAN_POINT('Ctrl Pts',(-0.254134067300259,-5.31377926402143,
2.35497740013087));
#70152=CARTESIAN_POINT('Ctrl Pts',(-4.57227750472522,-2.71939796778984,
2.1979789067888));
#70153=CARTESIAN_POINT('Ctrl Pts',(-4.79048620199859,2.31344428926255,2.04098041344675));
#70154=CARTESIAN_POINT('Ctrl Pts',(-0.713117253133846,5.27184368256949,
1.88398192010469));
#70155=CARTESIAN_POINT('Ctrl Pts',(4.00372781637104,3.50301057429394,1.72698342676264));
#70156=CARTESIAN_POINT('Ctrl Pts',(5.13040418378061,-1.40692656966539,1.56998493342058));
#70157=CARTESIAN_POINT('Ctrl Pts',(1.65679346991308,-5.05532001832255,1.41298644007852));
#70158=CARTESIAN_POINT('Ctrl Pts',(-3.30265813277885,-4.17057554901314,
1.25598794673646));
#70159=CARTESIAN_POINT('Ctrl Pts',(-5.30024450706594,0.453757243049607,
1.0989894533944));
#70160=CARTESIAN_POINT('Ctrl Pts',(-2.54590251921605,4.67146907303194,0.941990960052346));
#70161=CARTESIAN_POINT('Ctrl Pts',(2.49279148335452,4.69981123962122,0.784992466710289));
#70162=CARTESIAN_POINT('Ctrl Pts',(5.29341363228488,0.514825939282724,0.62799397336823));
#70163=CARTESIAN_POINT('Ctrl Pts',(3.35287346845927,-4.13364942235117,0.470995480026172));
#70164=CARTESIAN_POINT('Ctrl Pts',(-1.60471517422276,-5.07185789283195,
0.313996986684116));
#70165=CARTESIAN_POINT('Ctrl Pts',(-4.51864557778723,-2.07044823623904,
0.183164908899067));
#70166=CARTESIAN_POINT('Ctrl Pts',(-4.58920984496997,1.00349320106954,0.07849924667103));
#70167=CARTESIAN_POINT('Ctrl Pts',(-3.91646501574703,2.37129788193743,0.0261664155570096));
#70168=CARTESIAN_POINT('Ctrl Pts',(-3.43378788736191,2.93584158412995,0.));
#70169=CARTESIAN_POINT('Ctrl Pts',(-3.43378788736191,2.93584158412995,0.));
#70170=CARTESIAN_POINT('Ctrl Pts',(-3.52723777670969,2.83914483717434,2.20957577510153E-16));
#70171=CARTESIAN_POINT('Ctrl Pts',(-3.61593961326928,2.73846171784274,-1.95102593779902E-16));
#70172=CARTESIAN_POINT('Ctrl Pts',(-3.69983889649088,2.63418997519716,-5.55111512312578E-17));
#70173=CARTESIAN_POINT('Ctrl Pts',(-3.78516004991503,2.5281511032253,8.64459958272222E-17));
#70174=CARTESIAN_POINT('Ctrl Pts',(-3.86551489177621,2.41840048478536,3.57207213678775E-15));
#70175=CARTESIAN_POINT('Ctrl Pts',(-3.9408148769991,2.30531248881791,3.33066907387547E-15));
#70176=CARTESIAN_POINT('Ctrl Pts',(-4.01713525064214,2.19069203993958,3.08599476344226E-15));
#70177=CARTESIAN_POINT('Ctrl Pts',(-4.08826327828892,2.07264261686327,1.15541512747695E-15));
#70178=CARTESIAN_POINT('Ctrl Pts',(-4.15406859699169,1.95151684254046,1.38777878078145E-15));
#70179=CARTESIAN_POINT('Ctrl Pts',(-4.21980984783224,1.8305089959106,1.61991620552547E-15));
#70180=CARTESIAN_POINT('Ctrl Pts',(-4.28023911511666,1.70643015108279,2.039107624704E-15));
#70181=CARTESIAN_POINT('Ctrl Pts',(-4.33518267922297,1.57960398874639,2.4980018054066E-15));
#70182=CARTESIAN_POINT('Ctrl Pts',(-4.35306946209471,1.53831594955441,2.64739401730341E-15));
#70183=CARTESIAN_POINT('Ctrl Pts',(-4.37037449182742,1.49673656482301,-1.24977233183131E-15));
#70184=CARTESIAN_POINT('Ctrl Pts',(-4.38709067099901,1.45487653718474,-1.55431223447522E-15));
#70185=CARTESIAN_POINT('Ctrl Pts',(-4.39375920070266,1.43817745572383,-1.67580132393046E-15));
#70186=CARTESIAN_POINT('Ctrl Pts',(-4.40033069663165,1.42144199284245,2.13318250051857E-15));
#70187=CARTESIAN_POINT('Ctrl Pts',(-4.40680423707264,1.40467289792598,2.1094237467878E-15));
#70188=CARTESIAN_POINT('Ctrl Pts',(-4.45933329243635,1.26860134275516,1.91663513266347E-15));
#70189=CARTESIAN_POINT('Ctrl Pts',(-4.50543275765374,1.13027759164836,2.92434253228364E-15));
#70190=CARTESIAN_POINT('Ctrl Pts',(-4.54499128400339,0.990129694249863,
2.63677968348475E-15));
#70191=CARTESIAN_POINT('Ctrl Pts',(-4.58298351161253,0.855530878059325,
2.35904680574097E-15));
#70192=CARTESIAN_POINT('Ctrl Pts',(-4.61494272389214,0.719248781594657,
4.48491542532579E-15));
#70193=CARTESIAN_POINT('Ctrl Pts',(-4.64084676847695,0.58176526830246,3.3584246494911E-15));
#70194=CARTESIAN_POINT('Ctrl Pts',(-4.66691254514768,0.44342337572085,2.22490062051545E-15));
#70195=CARTESIAN_POINT('Ctrl Pts',(-4.68684755285248,0.303864196021266,
1.79312284184644E-16));
#70196=CARTESIAN_POINT('Ctrl Pts',(-4.70058040711193,0.163559265384357,
-6.66133814775094E-16));
#70197=CARTESIAN_POINT('Ctrl Pts',(-4.71271438319262,0.0395896491496948,
-1.41314696648225E-15));
#70198=CARTESIAN_POINT('Ctrl Pts',(-4.72000573130037,-0.0849628385647041,
1.44014651394631E-16));
#70199=CARTESIAN_POINT('Ctrl Pts',(-4.7223714742082,-0.209777558646538,
-3.88578058618805E-16));
#70200=CARTESIAN_POINT('Ctrl Pts',(-4.72292774412613,-0.239125918464476,
-5.13809461450429E-16));
#70201=CARTESIAN_POINT('Ctrl Pts',(-4.72321154151185,-0.268488777105225,
3.0010215925102E-15));
#70202=CARTESIAN_POINT('Ctrl Pts',(-4.72322152198113,-0.297861955465308,
2.91433543964104E-15));
#70203=CARTESIAN_POINT('Ctrl Pts',(-4.72322914092456,-0.320285007726138,
2.84816050575247E-15));
#70204=CARTESIAN_POINT('Ctrl Pts',(-4.72307708136321,-0.342716335801155,
3.67219762837691E-17));
#70205=CARTESIAN_POINT('Ctrl Pts',(-4.72276525050185,-0.365131269043745,
1.38777878078145E-16));
#70206=CARTESIAN_POINT('Ctrl Pts',(-4.72077152616445,-0.508443568958217,
7.91283323787342E-16));
#70207=CARTESIAN_POINT('Ctrl Pts',(-4.71225224775121,-0.651283769357607,
4.69641391259678E-15));
#70208=CARTESIAN_POINT('Ctrl Pts',(-4.69718724960338,-0.793159785562181,
4.52415882534751E-15));
#70209=CARTESIAN_POINT('Ctrl Pts',(-4.68213033873543,-0.934959639059055,
4.35199620907545E-15));
#70210=CARTESIAN_POINT('Ctrl Pts',(-4.66053490666648,-1.07579720961356,
2.29755459169068E-15));
#70211=CARTESIAN_POINT('Ctrl Pts',(-4.63233047059339,-1.21519245994795,
1.88737914186277E-15));
#70212=CARTESIAN_POINT('Ctrl Pts',(-4.62518265294206,-1.25051923720629,
1.78342885146082E-15));
#70213=CARTESIAN_POINT('Ctrl Pts',(-4.61761010448178,-1.28575339934606,
3.86113148383421E-16));
#70214=CARTESIAN_POINT('Ctrl Pts',(-4.60961114292865,-1.32088714489269,
2.22044604925031E-16));
#70215=CARTESIAN_POINT('Ctrl Pts',(-4.57836306126197,-1.45813772958496,
-4.20462921062943E-16));
#70216=CARTESIAN_POINT('Ctrl Pts',(-4.54061164386395,-1.59385666227503,
-3.37562086541692E-16));
#70217=CARTESIAN_POINT('Ctrl Pts',(-4.49667838831439,-1.72776655308613,
-8.04911692853238E-16));
#70218=CARTESIAN_POINT('Ctrl Pts',(-4.46792839524171,-1.81539740094895,
-1.11074602668306E-15));
#70219=CARTESIAN_POINT('Ctrl Pts',(-4.43652997184098,-1.90225339638272,
9.54490265544014E-16));
#70220=CARTESIAN_POINT('Ctrl Pts',(-4.40256174565587,-1.98825353803286,
7.21644966006352E-16));
#70221=CARTESIAN_POINT('Ctrl Pts',(-4.39065014752274,-2.01841110708421,
6.3999337724903E-16));
#70222=CARTESIAN_POINT('Ctrl Pts',(-4.37842246733328,-2.04846340327406,
1.30054899424822E-15));
#70223=CARTESIAN_POINT('Ctrl Pts',(-4.3658818524655,-2.07840682871088,1.27675647831893E-15));
#70224=CARTESIAN_POINT('Ctrl Pts',(-4.35886905063707,-2.09515140709612,
1.26345153267066E-15));
#70225=CARTESIAN_POINT('Ctrl Pts',(-4.35175838797214,-2.11186193915223,
-4.29181623021427E-15));
#70226=CARTESIAN_POINT('Ctrl Pts',(-4.34455039841696,-2.12853778716716,
-4.44089209850063E-15));
#70227=CARTESIAN_POINT('Ctrl Pts',(-4.33665307152192,-2.14680843281913,
-4.60422486348398E-15));
#70228=CARTESIAN_POINT('Ctrl Pts',(-4.3286424353965,-2.16502924396809,5.30168465333661E-15));
#70229=CARTESIAN_POINT('Ctrl Pts',(-4.32052144132994,-2.18319526042712,
5.16253706450698E-15));
#70230=CARTESIAN_POINT('Ctrl Pts',(-4.26272706163057,-2.31247668142725,
4.17227053836974E-15));
#70231=CARTESIAN_POINT('Ctrl Pts',(-4.19931793630604,-2.4390523089761,-3.17224447424671E-16));
#70232=CARTESIAN_POINT('Ctrl Pts',(-4.1306671181063,-2.56266098762457,-5.55111512312578E-17));
#70233=CARTESIAN_POINT('Ctrl Pts',(-4.0593379123478,-2.69109221545352,2.16412797287518E-16));
#70234=CARTESIAN_POINT('Ctrl Pts',(-3.9823498940757,-2.81632115639891,3.16344549884833E-15));
#70235=CARTESIAN_POINT('Ctrl Pts',(-3.90006549167258,-2.93804355166681,
2.74780198594726E-15));
#70236=CARTESIAN_POINT('Ctrl Pts',(-3.81789453604086,-3.05959812639587,
2.33273152715138E-15));
#70237=CARTESIAN_POINT('Ctrl Pts',(-3.73044127702168,-3.17765647132671,
1.52792430062925E-15));
#70238=CARTESIAN_POINT('Ctrl Pts',(-3.63801734753769,-3.29189441139934,
2.04003480774873E-15));
#70239=CARTESIAN_POINT('Ctrl Pts',(-3.56858774848175,-3.37771087062696,
2.42473633883647E-15));
#70240=CARTESIAN_POINT('Ctrl Pts',(-3.49635207705255,-3.46137105631218,
2.6380387160668E-15));
#70241=CARTESIAN_POINT('Ctrl Pts',(-3.42142672585507,-3.54272626619495,
2.95596880306448E-15));
#70242=CARTESIAN_POINT('Ctrl Pts',(-3.38629422705786,-3.58087372586878,
3.10504622773483E-15));
#70243=CARTESIAN_POINT('Ctrl Pts',(-3.3505701767281,-3.61851424013804,2.76570113010457E-15));
#70244=CARTESIAN_POINT('Ctrl Pts',(-3.31426568073248,-3.6556315716941,2.76167977375508E-15));
#70245=CARTESIAN_POINT('Ctrl Pts',(-3.29921135129803,-3.67102295839838,
2.76001224411176E-15));
#70246=CARTESIAN_POINT('Ctrl Pts',(-3.2840555690535,-3.68632600746954,3.617329513469E-16));
#70247=CARTESIAN_POINT('Ctrl Pts',(-3.26880440302003,-3.70153424964867,
5.13478148889135E-16));
#70248=CARTESIAN_POINT('Ctrl Pts',(-3.16314622619418,-3.8068950553632,1.56474995848081E-15));
#70249=CARTESIAN_POINT('Ctrl Pts',(-3.05312027550677,-3.90750387615403,
1.50739186887073E-15));
#70250=CARTESIAN_POINT('Ctrl Pts',(-2.93906465882528,-4.00303742675364,
1.35308431126191E-15));
#70251=CARTESIAN_POINT('Ctrl Pts',(-2.83344548104308,-4.09150457426047,
1.21019053860593E-15));
#70252=CARTESIAN_POINT('Ctrl Pts',(-2.72436990580127,-4.17561968062982,
2.13759783489021E-15));
#70253=CARTESIAN_POINT('Ctrl Pts',(-2.61207533410326,-4.25510133080791,
2.0122792321331E-15));
#70254=CARTESIAN_POINT('Ctrl Pts',(-2.56057702495619,-4.29155162872077,
1.95480810018898E-15));
#70255=CARTESIAN_POINT('Ctrl Pts',(-2.50840133628958,-4.32702707245024,
2.36751160669112E-15));
#70256=CARTESIAN_POINT('Ctrl Pts',(-2.45556938566372,-4.36149843071932,
2.75474087985117E-15));
#70257=CARTESIAN_POINT('Ctrl Pts',(-2.42827777589571,-4.37930543664865,
2.95477343758642E-15));
#70258=CARTESIAN_POINT('Ctrl Pts',(-2.40081102655259,-4.39684448061502,
1.19861602340893E-15));
#70259=CARTESIAN_POINT('Ctrl Pts',(-2.3731719452944,-4.41411137781326,1.24206200879939E-15));
#70260=CARTESIAN_POINT('Ctrl Pts',(-2.35240993886931,-4.42708197648195,
1.27469789200386E-15));
#70261=CARTESIAN_POINT('Ctrl Pts',(-2.3315588675056,-4.43989388919032,-2.42681870829991E-15));
#70262=CARTESIAN_POINT('Ctrl Pts',(-2.310621268056,-4.45254499954709,-2.38004060904018E-15));
#70263=CARTESIAN_POINT('Ctrl Pts',(-2.18359867883944,-4.52929576545271,
-2.09625089852901E-15));
#70264=CARTESIAN_POINT('Ctrl Pts',(-2.0533809663479,-4.60013945799199,1.86447051626453E-17));
#70265=CARTESIAN_POINT('Ctrl Pts',(-1.92026980955225,-4.66473533433833,
-1.2490009027033E-16));
#70266=CARTESIAN_POINT('Ctrl Pts',(-1.7911873441691,-4.72737617657195,-2.64100413770296E-16));
#70267=CARTESIAN_POINT('Ctrl Pts',(-1.65938332691157,-4.78414205363558,
1.04097051092433E-15));
#70268=CARTESIAN_POINT('Ctrl Pts',(-1.52510574125302,-4.83468405991464,
1.71217207078911E-15));
#70269=CARTESIAN_POINT('Ctrl Pts',(-1.45664804130053,-4.8604514989394,2.07094871730909E-15));
#70270=CARTESIAN_POINT('Ctrl Pts',(-1.38754702424773,-4.88460057019718,
-4.86141022577448E-16));
#70271=CARTESIAN_POINT('Ctrl Pts',(-1.31785621200041,-4.90714516622019,
-4.9960036108132E-16));
#70272=CARTESIAN_POINT('Ctrl Pts',(-4.51483246697105,0.00361950456559231,
7.11258330249198));
#70273=CARTESIAN_POINT('Ctrl Pts',(-4.5183463327351,0.455094042321683,7.09669960179219));
#70274=CARTESIAN_POINT('Ctrl Pts',(-4.45593254783999,0.905622974345749,
7.08081590109239));
#70275=CARTESIAN_POINT('Ctrl Pts',(-4.32353239297286,1.33455648409566,7.0649322003926));
#70276=CARTESIAN_POINT('Ctrl Pts',(-3.88730691409435,2.74778538768327,7.01259936927858));
#70277=CARTESIAN_POINT('Ctrl Pts',(-2.69135272588913,3.92658775510004,6.96026653816456));
#70278=CARTESIAN_POINT('Ctrl Pts',(-1.27193484569267,4.34236679115612,6.90793370705054));
#70279=CARTESIAN_POINT('Ctrl Pts',(0.147483034503799,4.75814582721219,6.85560087593652));
#70280=CARTESIAN_POINT('Ctrl Pts',(1.7903646066915,4.41090153190756,6.8032680448225));
#70281=CARTESIAN_POINT('Ctrl Pts',(2.92016317867997,3.45636397543961,6.75093521370848));
#70282=CARTESIAN_POINT('Ctrl Pts',(4.04996175066844,2.50182641897166,6.69860238259446));
#70283=CARTESIAN_POINT('Ctrl Pts',(4.66667732245768,0.939995601340394,6.64626955148044));
#70284=CARTESIAN_POINT('Ctrl Pts',(4.49379055447605,-0.528910651078803,
6.59393672036643));
#70285=CARTESIAN_POINT('Ctrl Pts',(4.32090378649441,-1.997816903498,6.54160388925241));
#70286=CARTESIAN_POINT('Ctrl Pts',(3.35841467874189,-3.37379859070514,6.48927105813838));
#70287=CARTESIAN_POINT('Ctrl Pts',(2.03786057988447,-4.03992744750561,6.43693822702436));
#70288=CARTESIAN_POINT('Ctrl Pts',(0.717306481027035,-4.70605630430607,
6.38460539591034));
#70289=CARTESIAN_POINT('Ctrl Pts',(-0.961312608935302,-4.66233233069989,
6.33227256479632));
#70290=CARTESIAN_POINT('Ctrl Pts',(-2.24539882471135,-3.92836528976861,
6.27993973368231));
#70291=CARTESIAN_POINT('Ctrl Pts',(-3.5294850404874,-3.19439824883733,6.22760690256829));
#70292=CARTESIAN_POINT('Ctrl Pts',(-4.41903838207715,-1.77018814058096,
6.17527407145427));
#70293=CARTESIAN_POINT('Ctrl Pts',(-4.51522851969403,-0.294270927746662,
6.12294124034025));
#70294=CARTESIAN_POINT('Ctrl Pts',(-4.52157464089458,-0.196897644511263,
6.11948859439083));
#70295=CARTESIAN_POINT('Ctrl Pts',(-4.52446751475242,-0.0992992973699645,
6.1160359484414));
#70296=CARTESIAN_POINT('Ctrl Pts',(-4.52399690261043,-0.00167256832429505,
6.11258330249198));
#70297=CARTESIAN_POINT('Ctrl Pts',(-1.31303618635644,-4.90075024188323,
8.));
#70298=CARTESIAN_POINT('Ctrl Pts',(-1.45239709211802,-4.85517655769009,
8.));
#70299=CARTESIAN_POINT('Ctrl Pts',(-1.58927461952972,-4.80351078633936,
8.));
#70300=CARTESIAN_POINT('Ctrl Pts',(-1.72340721958534,-4.74604566824414,
8.));
#70301=CARTESIAN_POINT('Ctrl Pts',(-1.85924970425712,-4.68784800100459,
8.));
#70302=CARTESIAN_POINT('Ctrl Pts',(-1.99227741877149,-4.62370180241543,
8.));
#70303=CARTESIAN_POINT('Ctrl Pts',(-2.1221970609313,-4.55386234778148,8.));
#70304=CARTESIAN_POINT('Ctrl Pts',(-2.25246970806005,-4.48383313219911,
8.));
#70305=CARTESIAN_POINT('Ctrl Pts',(-2.37961793682551,-4.40807921917534,
8.));
#70306=CARTESIAN_POINT('Ctrl Pts',(-2.50331578855033,-4.32681572428032,
8.));
#70307=CARTESIAN_POINT('Ctrl Pts',(-2.62609342189428,-4.24615676827303,
8.));
#70308=CARTESIAN_POINT('Ctrl Pts',(-2.74547232113475,-4.16006940168606,
8.));
#70309=CARTESIAN_POINT('Ctrl Pts',(-2.86109611850811,-4.06872967104376,
8.));
#70310=CARTESIAN_POINT('Ctrl Pts',(-2.9021226048247,-4.0363198359191,8.));
#70311=CARTESIAN_POINT('Ctrl Pts',(-2.94267593191283,-4.00324843420239,
8.));
#70312=CARTESIAN_POINT('Ctrl Pts',(-2.98273884627905,-3.96952246026761,
8.));
#70313=CARTESIAN_POINT('Ctrl Pts',(-2.99980179304064,-3.95515844040447,
8.));
#70314=CARTESIAN_POINT('Ctrl Pts',(-3.01677686159523,-3.94067464141144,
8.));
#70315=CARTESIAN_POINT('Ctrl Pts',(-3.03364692784275,-3.92608549145045,
8.));
#70316=CARTESIAN_POINT('Ctrl Pts',(-3.14433906287484,-3.83035947983968,
8.));
#70317=CARTESIAN_POINT('Ctrl Pts',(-3.25067173076357,-3.72996938710921,
8.));
#70318=CARTESIAN_POINT('Ctrl Pts',(-3.35235942406226,-3.62515267891276,
8.));
#70319=CARTESIAN_POINT('Ctrl Pts',(-3.36192701172294,-3.61529068862227,
8.));
#70320=CARTESIAN_POINT('Ctrl Pts',(-3.37145345441303,-3.60538948288356,
8.));
#70321=CARTESIAN_POINT('Ctrl Pts',(-3.38093849819353,-3.5954492420827,8.));
#70322=CARTESIAN_POINT('Ctrl Pts',(-3.48179697338609,-3.48975046478426,
8.));
#70323=CARTESIAN_POINT('Ctrl Pts',(-3.57797791034191,-3.37964062514819,
8.));
#70324=CARTESIAN_POINT('Ctrl Pts',(-3.6691784190789,-3.26549870852508,8.));
#70325=CARTESIAN_POINT('Ctrl Pts',(-3.75971104108468,-3.1521926849539,8.));
#70326=CARTESIAN_POINT('Ctrl Pts',(-3.84533634314077,-3.03491270174392,
8.));
#70327=CARTESIAN_POINT('Ctrl Pts',(-3.92571335075401,-2.91400477707446,
8.));
#70328=CARTESIAN_POINT('Ctrl Pts',(-3.99657459670685,-2.80741103289235,
8.));
#70329=CARTESIAN_POINT('Ctrl Pts',(-4.06335624155544,-2.69799686623316,
8.));
#70330=CARTESIAN_POINT('Ctrl Pts',(-4.12579142887319,-2.5859898555039,8.));
#70331=CARTESIAN_POINT('Ctrl Pts',(-4.14218052019666,-2.55658827593677,
8.));
#70332=CARTESIAN_POINT('Ctrl Pts',(-4.15826993976141,-2.52700800600865,
8.));
#70333=CARTESIAN_POINT('Ctrl Pts',(-4.17405446883537,-2.49725311040552,
8.));
#70334=CARTESIAN_POINT('Ctrl Pts',(-4.18546373911311,-2.47574587097943,
8.));
#70335=CARTESIAN_POINT('Ctrl Pts',(-4.19671529109329,-2.45414413479639,
8.));
#70336=CARTESIAN_POINT('Ctrl Pts',(-4.20779517261687,-2.4324732839539,8.));
#70337=CARTESIAN_POINT('Ctrl Pts',(-4.27314976421176,-2.30464794545096,
8.));
#70338=CARTESIAN_POINT('Ctrl Pts',(-4.33262109126524,-2.17426237076666,
8.));
#70339=CARTESIAN_POINT('Ctrl Pts',(-4.38592494350939,-2.0416738299269,8.));
#70340=CARTESIAN_POINT('Ctrl Pts',(-4.43841400089354,-1.91111201805743,
8.));
#70341=CARTESIAN_POINT('Ctrl Pts',(-4.48492299905459,-1.7784133775905,8.));
#70342=CARTESIAN_POINT('Ctrl Pts',(-4.52513335521759,-1.64390172617838,
8.));
#70343=CARTESIAN_POINT('Ctrl Pts',(-4.537048107786,-1.60404450537571,8.));
#70344=CARTESIAN_POINT('Ctrl Pts',(-4.54840950403996,-1.5640280227951,8.));
#70345=CARTESIAN_POINT('Ctrl Pts',(-4.55920838150573,-1.52386053965931,
8.));
#70346=CARTESIAN_POINT('Ctrl Pts',(-4.59649237875198,-1.385179057684,8.));
#70347=CARTESIAN_POINT('Ctrl Pts',(-4.62707496138222,-1.24469748534875,
8.));
#70348=CARTESIAN_POINT('Ctrl Pts',(-4.65105491040296,-1.10285889077504,
8.));
#70349=CARTESIAN_POINT('Ctrl Pts',(-4.66554282028716,-1.017164597826,8.));
#70350=CARTESIAN_POINT('Ctrl Pts',(-4.67761961594462,-0.930974942162248,
8.));
#70351=CARTESIAN_POINT('Ctrl Pts',(-4.68729801221865,-0.844388845291519,
8.));
#70352=CARTESIAN_POINT('Ctrl Pts',(-4.69282817886049,-0.794914166739051,
8.));
#70353=CARTESIAN_POINT('Ctrl Pts',(-4.69757516967293,-0.745310079919106,
8.));
#70354=CARTESIAN_POINT('Ctrl Pts',(-4.70154039472519,-0.695595329877529,
8.));
#70355=CARTESIAN_POINT('Ctrl Pts',(-4.70301053775668,-0.677163136906814,
8.));
#70356=CARTESIAN_POINT('Ctrl Pts',(-4.70437287652954,-0.658719449757616,
8.));
#70357=CARTESIAN_POINT('Ctrl Pts',(-4.70562704431493,-0.64027493011297,
8.));
#70358=CARTESIAN_POINT('Ctrl Pts',(-4.71515809633756,-0.500105745165328,
8.));
#70359=CARTESIAN_POINT('Ctrl Pts',(-4.71845973908213,-0.359723770205855,
8.));
#70360=CARTESIAN_POINT('Ctrl Pts',(-4.71568669686701,-0.219543283976319,
8.));
#70361=CARTESIAN_POINT('Ctrl Pts',(-4.71286811953556,-0.0770609450327588,
8.));
#70362=CARTESIAN_POINT('Ctrl Pts',(-4.70377361453064,0.0652140588645918,
8.));
#70363=CARTESIAN_POINT('Ctrl Pts',(-4.68851230252744,0.206844911988138,
8.));
#70364=CARTESIAN_POINT('Ctrl Pts',(-4.67333458060724,0.347700016947462,
8.));
#70365=CARTESIAN_POINT('Ctrl Pts',(-4.65205714501789,0.487918806531984,
8.));
#70366=CARTESIAN_POINT('Ctrl Pts',(-4.62473814484182,0.627057654071025,
8.));
#70367=CARTESIAN_POINT('Ctrl Pts',(-4.605133388788,0.726906958439074,8.));
#70368=CARTESIAN_POINT('Ctrl Pts',(-4.5824162991499,0.826199852698566,8.));
#70369=CARTESIAN_POINT('Ctrl Pts',(-4.55659376741278,0.92476446952987,8.));
#70370=CARTESIAN_POINT('Ctrl Pts',(-4.54451944953447,0.97085214703918,8.));
#70371=CARTESIAN_POINT('Ctrl Pts',(-4.53176599217756,1.01678048248609,8.));
#70372=CARTESIAN_POINT('Ctrl Pts',(-4.5183332282825,1.06253124418397,8.));
#70373=CARTESIAN_POINT('Ctrl Pts',(-4.51267692512135,1.08179609392292,8.));
#70374=CARTESIAN_POINT('Ctrl Pts',(-4.50690016711964,1.10102945232834,8.));
#70375=CARTESIAN_POINT('Ctrl Pts',(-4.50100291315461,1.12022993263941,8.));
#70376=CARTESIAN_POINT('Ctrl Pts',(-4.49471977615854,1.14068678406554,8.));
#70377=CARTESIAN_POINT('Ctrl Pts',(-4.48830254703555,1.16109751332069,8.));
#70378=CARTESIAN_POINT('Ctrl Pts',(-4.48175248385615,1.18145762320509,8.));
#70379=CARTESIAN_POINT('Ctrl Pts',(-4.43884234970562,1.31483878649018,8.));
#70380=CARTESIAN_POINT('Ctrl Pts',(-4.39022235830023,1.4460911608231,8.));
#70381=CARTESIAN_POINT('Ctrl Pts',(-4.33596033524399,1.57478158992507,8.));
#70382=CARTESIAN_POINT('Ctrl Pts',(-4.28905827705606,1.68601677162324,8.));
#70383=CARTESIAN_POINT('Ctrl Pts',(-4.23794008569217,1.79533788193322,8.));
#70384=CARTESIAN_POINT('Ctrl Pts',(-4.18262262022186,1.90244778297798,8.));
#70385=CARTESIAN_POINT('Ctrl Pts',(-4.15876953368252,1.94863395071215,8.));
#70386=CARTESIAN_POINT('Ctrl Pts',(-4.13413534457581,1.9944087336574,8.));
#70387=CARTESIAN_POINT('Ctrl Pts',(-4.10872005342092,2.03974709902823,8.));
#70388=CARTESIAN_POINT('Ctrl Pts',(-4.09757333138634,2.05963174851782,8.));
#70389=CARTESIAN_POINT('Ctrl Pts',(-4.08627634995272,2.07943244040586,8.));
#70390=CARTESIAN_POINT('Ctrl Pts',(-4.0748290615074,2.09914701235749,8.));
#70391=CARTESIAN_POINT('Ctrl Pts',(-4.06286920268517,2.11974433533126,8.));
#70392=CARTESIAN_POINT('Ctrl Pts',(-4.05074975381766,2.1402399100487,8.));
#70393=CARTESIAN_POINT('Ctrl Pts',(-4.0384724823486,2.16062907002492,8.));
#70394=CARTESIAN_POINT('Ctrl Pts',(-3.96920273979072,2.27566699731059,8.));
#70395=CARTESIAN_POINT('Ctrl Pts',(-3.89489711290362,2.38734570786034,8.));
#70396=CARTESIAN_POINT('Ctrl Pts',(-3.81559004701476,2.49525769668179,8.));
#70397=CARTESIAN_POINT('Ctrl Pts',(-3.739663695997,2.59856959519238,8.));
#70398=CARTESIAN_POINT('Ctrl Pts',(-3.65915281331369,2.69842939750744,8.));
#70399=CARTESIAN_POINT('Ctrl Pts',(-3.57405581868196,2.79444797267076,8.));
#70400=CARTESIAN_POINT('Ctrl Pts',(-3.53072763156913,2.8433370175658,8.));
#70401=CARTESIAN_POINT('Ctrl Pts',(-3.48620998149697,2.89122965827726,8.));
#70402=CARTESIAN_POINT('Ctrl Pts',(-3.44054916109509,2.93810681611542,8.));
#70403=CARTESIAN_POINT('Origin',(-1.11022302462516E-15,0.,8.));
#70404=CARTESIAN_POINT('',(4.90747728811182,-8.5,8.));
#70405=CARTESIAN_POINT('',(9.81495457622364,0.,8.));
#70406=CARTESIAN_POINT('',(4.90747728811182,-8.5,8.));
#70407=CARTESIAN_POINT('',(4.90747728811182,8.5,8.));
#70408=CARTESIAN_POINT('',(9.81495457622364,0.,8.));
#70409=CARTESIAN_POINT('',(-4.90747728811182,8.5,8.));
#70410=CARTESIAN_POINT('',(4.90747728811182,8.5,8.));
#70411=CARTESIAN_POINT('',(-9.81495457622364,1.11022302462516E-15,8.));
#70412=CARTESIAN_POINT('',(-4.90747728811182,8.5,8.));
#70413=CARTESIAN_POINT('',(-4.90747728811182,-8.5,8.));
#70414=CARTESIAN_POINT('',(-9.81495457622364,1.20198527055489E-15,8.));
#70415=CARTESIAN_POINT('',(-4.90747728811182,-8.5,8.));
#70416=CARTESIAN_POINT('Origin',(0.,0.,4.));
#70417=CARTESIAN_POINT('Origin',(-4.90747728811182,-8.5,0.));
#70418=CARTESIAN_POINT('',(-4.90747728811182,-8.5,0.));
#70419=CARTESIAN_POINT('',(4.90747728811182,-8.5,0.));
#70420=CARTESIAN_POINT('',(-4.90747728811182,-8.5,0.));
#70421=CARTESIAN_POINT('',(4.90747728811182,-8.5,0.));
#70422=CARTESIAN_POINT('',(-4.90747728811182,-8.5,0.));
#70423=CARTESIAN_POINT('Origin',(-9.81495457622364,1.20198527055489E-15,
0.));
#70424=CARTESIAN_POINT('',(-9.81495457622364,1.20198527055489E-15,0.));
#70425=CARTESIAN_POINT('',(-9.81495457622364,1.20198527055489E-15,0.));
#70426=CARTESIAN_POINT('',(-9.81495457622364,1.20198527055489E-15,0.));
#70427=CARTESIAN_POINT('Origin',(-4.90747728811182,8.5,0.));
#70428=CARTESIAN_POINT('',(-4.90747728811182,8.5,0.));
#70429=CARTESIAN_POINT('',(-4.90747728811182,8.5,0.));
#70430=CARTESIAN_POINT('',(-4.90747728811182,8.5,0.));
#70431=CARTESIAN_POINT('Origin',(4.90747728811182,8.5,0.));
#70432=CARTESIAN_POINT('',(4.90747728811182,8.5,0.));
#70433=CARTESIAN_POINT('',(4.90747728811182,8.5,0.));
#70434=CARTESIAN_POINT('',(4.90747728811182,8.5,0.));
#70435=CARTESIAN_POINT('Origin',(9.81495457622364,0.,0.));
#70436=CARTESIAN_POINT('',(9.81495457622364,0.,0.));
#70437=CARTESIAN_POINT('',(9.81495457622364,0.,0.));
#70438=CARTESIAN_POINT('',(9.81495457622364,0.,0.));
#70439=CARTESIAN_POINT('Origin',(4.90747728811182,-8.5,0.));
#70440=CARTESIAN_POINT('',(4.90747728811182,-8.5,0.));
#70441=CARTESIAN_POINT('Origin',(-1.11022302462516E-15,0.,0.));
#97445=UNCERTAINTY_MEASURE_WITH_UNIT(LENGTH_MEASURE(0.01),#97476,
'DISTANCE_ACCURACY_VALUE',
'Maximum model space distance between geometric entities at asserted c
onnectivities');
#97452=UNCERTAINTY_MEASURE_WITH_UNIT(LENGTH_MEASURE(0.01),#97476,
'DISTANCE_ACCURACY_VALUE',
'Maximum model space distance between geometric entities at asserted c
onnectivities');
#97468=(
GEOMETRIC_REPRESENTATION_CONTEXT(3)
GLOBAL_UNCERTAINTY_ASSIGNED_CONTEXT((#97445))
GLOBAL_UNIT_ASSIGNED_CONTEXT((#97476,#97478,#97479))
REPRESENTATION_CONTEXT('','3D')
);
#97475=(
GEOMETRIC_REPRESENTATION_CONTEXT(3)
GLOBAL_UNCERTAINTY_ASSIGNED_CONTEXT((#97452))
GLOBAL_UNIT_ASSIGNED_CONTEXT((#97476,#97478,#97479))
REPRESENTATION_CONTEXT('','3D')
);
#97476=(
LENGTH_UNIT()
NAMED_UNIT(*)
SI_UNIT(.MILLI.,.METRE.)
);
#97478=(
NAMED_UNIT(*)
PLANE_ANGLE_UNIT()
SI_UNIT($,.RADIAN.)
);
#97479=(
NAMED_UNIT(*)
SI_UNIT($,.STERADIAN.)
SOLID_ANGLE_UNIT()
);
#97495=SHAPE_DEFINITION_REPRESENTATION(#97557,#97618);
#97557=PRODUCT_DEFINITION_SHAPE('',$,#97641);
#97618=SHAPE_REPRESENTATION('',(#22950),#97468);
#97625=PRODUCT_DEFINITION_CONTEXT('part definition',#97693,'design');
#97641=PRODUCT_DEFINITION('Lock nut M10','Lock nut M10',#97663,#97625);
#97663=PRODUCT_DEFINITION_FORMATION('',$,#97710);
#97693=APPLICATION_CONTEXT(
'Core Data for Automotive Mechanical Design Process');
#97694=PRODUCT_CONTEXT('part definition',#97693,'mechanical');
#97710=PRODUCT('Lock nut M10','Lock nut M10',$,(#97694));
#97722=PRESENTATION_STYLE_ASSIGNMENT((#97729));
#97729=SURFACE_STYLE_USAGE(.BOTH.,#97736);
#97736=SURFACE_SIDE_STYLE('',(#97743));
#97743=SURFACE_STYLE_FILL_AREA(#97750);
#97750=FILL_AREA_STYLE('Gray',(#97757));
#97757=FILL_AREA_STYLE_COLOUR('Gray',#97764);
#97764=COLOUR_RGB('Gray',0.407843137254902,0.447058823529412,0.498039215686275);
ENDSEC;
END-ISO-10303-21;
